ISO-10303-21;
HEADER;
FILE_DESCRIPTION (('STEP AP214'),
    '1' );
FILE_NAME ('Rod.step',
    '2026-10-28T16:39:03',
    ( '' ),
    ( '' ),
    'SwSTEP 2.0',
    'SolidWorks 2024',
    '' );
FILE_SCHEMA (( 'AUTOMOTIVE_DESIGN' ));
ENDSEC;

DATA;
#1=VERTEX_POINT ( 'NONE', #6487 ) ;
#3=CARTESIAN_POINT ( 'NONE',  ( 375.4247212639274380, -15.61249499599598956, 12.50000000000000533 ) ) ;
#4=ADVANCED_FACE ( 'NONE', ( #7050 ), #2111, .F. ) ;
#9=CARTESIAN_POINT ( 'NONE',  ( 387.3898630172379285, 19.93132096080314497, 1.708129828930195826 ) ) ;
#12=AXIS2_PLACEMENT_3D ( 'NONE', #2676, #866, #3439 ) ;
#13=DIRECTION ( 'NONE',  ( -1.000000000000000000, -0.000000000000000000, -0.000000000000000000 ) ) ;
#27=CARTESIAN_POINT ( 'NONE',  ( 371.6961001703501211, 15.95358756117676258, -12.06260739558933714 ) ) ;
#29=CARTESIAN_POINT ( 'NONE',  ( 368.6956339375703351, -16.83403191367835561, 10.80131548116625417 ) ) ;
#31=LINE ( 'NONE', #3054, #2794 ) ;
#37=CARTESIAN_POINT ( 'NONE',  ( 376.6870407283136046, -15.69785030319133945, 12.39275847443047773 ) ) ;
#63=ORIENTED_EDGE ( 'NONE', *, *, #3507, .F. ) ;
#64=CARTESIAN_POINT ( 'NONE',  ( 370.5187250548066231, 16.23897639391231706, -11.67616422689687639 ) ) ;
#65=ORIENTED_EDGE ( 'NONE', *, *, #7166, .T. ) ;
#66=CARTESIAN_POINT ( 'NONE',  ( 364.2065580935995968, -18.97653311414304511, 6.355249004872655760 ) ) ;
#68=EDGE_CURVE ( 'NONE', #6240, #2057, #7224, .T. ) ;
#70=VECTOR ( 'NONE', #486, 999.9999999999998863 ) ;
#86=VECTOR ( 'NONE', #7226, 1000.000000000000000 ) ;
#94=( LENGTH_UNIT ( ) NAMED_UNIT ( * ) SI_UNIT ( .MILLI., .METRE. ) );
#105=VECTOR ( 'NONE', #3844, 1000.000000000000000 ) ;
#119=EDGE_LOOP ( 'NONE', ( #1348, #4627 ) ) ;
#122=CARTESIAN_POINT ( 'NONE',  ( 375.8519756245596568, -15.61249499599599311, -12.50000000000000000 ) ) ;
#136=VERTEX_POINT ( 'NONE', #4752 ) ;
#148=CARTESIAN_POINT ( 'NONE',  ( 362.5886599408613051, 19.94427247194493802, -1.702902647306309358 ) ) ;
#153=CARTESIAN_POINT ( 'NONE',  ( 0.000000000000000000, 15.00000000000000000, 0.000000000000000000 ) ) ;
#159=CYLINDRICAL_SURFACE ( 'NONE', #2014, 12.50000000000000355 ) ;
#160=CARTESIAN_POINT ( 'NONE',  ( 376.6830312554756688, -15.68244000841234964, -12.41390036673199759 ) ) ;
#167=DIRECTION ( 'NONE',  ( -1.000000000000000000, -0.000000000000000000, -0.000000000000000000 ) ) ;
#173=ORIENTED_EDGE ( 'NONE', *, *, #2685, .F. ) ;
#190=EDGE_CURVE ( 'NONE', #6276, #982, #5318, .T. ) ;
#194=CARTESIAN_POINT ( 'NONE',  ( 400.0000000000000000, -12.50000000000000000, -12.95183384698871798 ) ) ;
#196=AXIS2_PLACEMENT_3D ( 'NONE', #5443, #2356, #6569 ) ;
#203=ADVANCED_FACE ( 'NONE', ( #4230 ), #7485, .T. ) ;
#210=DIRECTION ( 'NONE',  ( 0.000000000000000000, 0.000000000000000000, 1.000000000000000000 ) ) ;
#215=ORIENTED_EDGE ( 'NONE', *, *, #2036, .F. ) ;
#223=ADVANCED_FACE ( 'NONE', ( #5439 ), #6682, .T. ) ;
#228=ORIENTED_EDGE ( 'NONE', *, *, #5969, .F. ) ;
#239=DIRECTION ( 'NONE',  ( 0.7071067811865517916, 8.659560562354879857E-17, 0.7071067811865431318 ) ) ;
#249=CIRCLE ( 'NONE', #2019, 12.50000000000000355 ) ;
#261=DIRECTION ( 'NONE',  ( 0.000000000000000000, 0.000000000000000000, 1.000000000000000000 ) ) ;
#270=DIRECTION ( 'NONE',  ( -1.000000000000000000, -0.000000000000000000, -0.000000000000000000 ) ) ;
#281=DIRECTION ( 'NONE',  ( -1.000000000000000000, -0.000000000000000000, -0.000000000000000000 ) ) ;
#290=CARTESIAN_POINT ( 'NONE',  ( 375.0000000000000000, 15.61249499599599488, -12.50000000000000000 ) ) ;
#322=VERTEX_POINT ( 'NONE', #2469 ) ;
#329=CARTESIAN_POINT ( 'NONE',  ( 383.2533226507719633, 17.65289753843946841, 9.421765557058566998 ) ) ;
#349=DIRECTION ( 'NONE',  ( 0.000000000000000000, 0.000000000000000000, 1.000000000000000000 ) ) ;
#359=VECTOR ( 'NONE', #798, 999.9999999999998863 ) ;
#373=CARTESIAN_POINT ( 'NONE',  ( 386.8096635605198230, 19.57571528166833019, 4.117265725333339788 ) ) ;
#382=DIRECTION ( 'NONE',  ( 0.000000000000000000, 0.000000000000000000, -1.000000000000000000 ) ) ;
#388=B_SPLINE_CURVE_WITH_KNOTS ( 'NONE', 3,
 ( #7794, #5299, #2264, #927, #4425, #2865, #3378, #460, #2907, #5344, #6884, #5829, #329, #2176, #4613, #7071, #1569, #974, #3423, #5867, #373, #7710, #5258, #4652, #9, #2458, #2307, #4173, #7314, #4736, #7196, #2339, #6032, #3068, #7831, #2951, #4892, #4770, #6109, #1730, #3664, #5507, #7232, #5989, #6629, #1692, #1130, #7903, #616, #501, #1812, #538, #3584, #2418 ),
 .UNSPECIFIED., .F., .F.,
 ( 4, 2, 2, 2, 2, 2, 2, 2, 2, 2, 2, 2, 2, 2, 2, 2, 2, 2, 2, 2, 2, 2, 2, 2, 2, 2, 4 ),
 ( 0.04018604478735846031, 0.04269101871805709714, 0.04394350568340633229, 0.04519599264875557437, 0.04644847961410480952, 0.04770096657945405161, 0.05020594051015265374, 0.05145842747550190277, 0.05271091444085115874, 0.05521588837154975393, 0.05646837533689905153, 0.05772086230224834913, 0.05897334926759764673, 0.06022583623294694433, 0.06273081016364553952, 0.06398329712899483712, 0.06523578409434413472, 0.06648827105969341844, 0.06774075802504271604, 0.07024573195574131124, 0.07149821892109066435, 0.07275070588644001746, 0.07525567981713872368, 0.07650816678248806291, 0.07776065374783742989, 0.07901314071318678300, 0.08026562767853613611 ),
 .UNSPECIFIED. ) ;
#432=FACE_OUTER_BOUND ( 'NONE', #1200, .T. ) ;
#451=ORIENTED_EDGE ( 'NONE', *, *, #4286, .T. ) ;
#460=CARTESIAN_POINT ( 'NONE',  ( 380.2287650028787880, 16.46093790404528789, 11.36110438390628197 ) ) ;
#462=CARTESIAN_POINT ( 'NONE',  ( 400.0000000000000000, 12.50000000000000000, 12.95183384698871620 ) ) ;
#465=DIRECTION ( 'NONE',  ( 0.000000000000000000, 0.000000000000000000, 1.000000000000000000 ) ) ;
#480=EDGE_CURVE ( 'NONE', #3444, #2321, #3270, .T. ) ;
#485=ORIENTED_EDGE ( 'NONE', *, *, #7101, .T. ) ;
#486=DIRECTION ( 'NONE',  ( -0.7071067811865479058, 8.659560562354930393E-17, -0.7071067811865472397 ) ) ;
#493=EDGE_LOOP ( 'NONE', ( #5975, #1539, #5084, #6737 ) ) ;
#501=CARTESIAN_POINT ( 'NONE',  ( 377.1106974111345380, 15.74939801616919866, -12.32751675873151598 ) ) ;
#508=AXIS2_PLACEMENT_3D ( 'NONE', #3751, #3075, #3787 ) ;
#517=CARTESIAN_POINT ( 'NONE',  ( 398.0000000000001137, 0.000000000000000000, 0.000000000000000000 ) ) ;
#523=CARTESIAN_POINT ( 'NONE',  ( 372.0751627177024830, -15.87901657654723664, -12.16010032319875833 ) ) ;
#529=ORIENTED_EDGE ( 'NONE', *, *, #2971, .F. ) ;
#532=DIRECTION ( 'NONE',  ( 0.000000000000000000, 0.000000000000000000, -1.000000000000000000 ) ) ;
#534=DIRECTION ( 'NONE',  ( 0.000000000000000000, 0.000000000000000000, -1.000000000000000000 ) ) ;
#536=( GEOMETRIC_REPRESENTATION_CONTEXT ( 3 ) GLOBAL_UNCERTAINTY_ASSIGNED_CONTEXT ( ( #5271 ) ) GLOBAL_UNIT_ASSIGNED_CONTEXT ( ( #94, #7442, #5550 ) ) REPRESENTATION_CONTEXT ( 'NONE', 'WORKASPACE' ) );
#538=CARTESIAN_POINT ( 'NONE',  ( 375.8507511021305163, 15.62998136526340076, -12.47825053757332370 ) ) ;
#557=CARTESIAN_POINT ( 'NONE',  ( 375.0000000000000000, -12.50000000000000355, -12.50000000000000000 ) ) ;
#560=CARTESIAN_POINT ( 'NONE',  ( 366.4515434226340176, -17.79791451299709948, -9.128686039268288255 ) ) ;
#566=CLOSED_SHELL ( 'NONE', ( #4803, #7833, #4, #588, #5189, #2945, #7825, #1974, #223, #578, #4507, #4448, #7790, #3968, #3765, #3719, #6908, #6228, #5216, #5664, #2044, #4485, #203, #6599 ) ) ;
#570=CARTESIAN_POINT ( 'NONE',  ( 382.6319868782507569, -17.37589182433591972, 9.907690019304302709 ) ) ;
#578=ADVANCED_FACE ( 'NONE', ( #1099 ), #6038, .F. ) ;
#583=CARTESIAN_POINT ( 'NONE',  ( 375.0000000000000000, -12.50000000000000355, 3.061616997868383043E-15 ) ) ;
#588=ADVANCED_FACE ( 'NONE', ( #7121 ), #4700, .F. ) ;
#594=ORIENTED_EDGE ( 'NONE', *, *, #4286, .F. ) ;
#596=CIRCLE ( 'NONE', #2906, 25.00000000000000000 ) ;
#599=DIRECTION ( 'NONE',  ( 1.000000000000000000, 0.000000000000000000, 0.000000000000000000 ) ) ;
#610=CARTESIAN_POINT ( 'NONE',  ( 382.3090924919189888, -17.23604965026853009, 10.14822696828370319 ) ) ;
#611=CARTESIAN_POINT ( 'NONE',  ( 387.4113400591389222, -19.94427247194493802, -1.702902647306309358 ) ) ;
#614=CARTESIAN_POINT ( 'NONE',  ( 190.0000000000000000, 12.50000000000000000, 21.65063509461096913 ) ) ;
#616=CARTESIAN_POINT ( 'NONE',  ( 377.9248372822975170, 15.87901657654723664, -12.16010032319875833 ) ) ;
#635=ORIENTED_EDGE ( 'NONE', *, *, #3722, .F. ) ;
#639=CARTESIAN_POINT ( 'NONE',  ( 371.6813660871608818, 15.95663992257128427, 12.05857923940197907 ) ) ;
#650=DIRECTION ( 'NONE',  ( 1.000000000000000000, 0.000000000000000000, 0.000000000000000000 ) ) ;
#670=ORIENTED_EDGE ( 'NONE', *, *, #5066, .T. ) ;
#681=CARTESIAN_POINT ( 'NONE',  ( 378.3186339128393456, -15.95663992257128427, 12.05857923940197907 ) ) ;
#682=CARTESIAN_POINT ( 'NONE',  ( 381.3105327226213035, -16.82862359362766469, -10.81999899256329911 ) ) ;
#690=CARTESIAN_POINT ( 'NONE',  ( 400.0000000000000000, 20.00000000000000000, 0.000000000000000000 ) ) ;
#700=LINE ( 'NONE', #3155, #3685 ) ;
#704=AXIS2_PLACEMENT_3D ( 'NONE', #5018, #167, #210 ) ;
#710=DIRECTION ( 'NONE',  ( -1.000000000000000000, -0.000000000000000000, -0.000000000000000000 ) ) ;
#718=EDGE_CURVE ( 'NONE', #1234, #1377, #2427, .T. ) ;
#725=CARTESIAN_POINT ( 'NONE',  ( 386.6633783623262843, -19.48763309926589216, -4.514690562563614229 ) ) ;
#726=DIRECTION ( 'NONE',  ( 0.000000000000000000, 0.000000000000000000, -1.000000000000000000 ) ) ;
#739=AXIS2_PLACEMENT_3D ( 'NONE', #5978, #5900, #1078 ) ;
#748=CARTESIAN_POINT ( 'NONE',  ( 372.0982571448921590, 15.87479745381989815, -12.16559770555248754 ) ) ;
#758=AXIS2_PLACEMENT_3D ( 'NONE', #6542, #5289, #4124 ) ;
#763=CARTESIAN_POINT ( 'NONE',  ( 375.0000000000000000, -15.61249499599599488, -12.50000000000000000 ) ) ;
#768=DIRECTION ( 'NONE',  ( 0.000000000000000000, -0.000000000000000000, 1.000000000000000000 ) ) ;
#771=LINE ( 'NONE', #3225, #4156 ) ;
#772=B_SPLINE_CURVE_WITH_KNOTS ( 'NONE', 3,
 ( #7335, #1945, #6284, #748, #27, #4429, #64, #1312, #2476, #6208, #3237, #3801, #1827, #1387, #3691, #5565, #3163, #3204, #5648, #2558, #3733, #148, #7375, #2441, #4387, #6727, #5030, #5000, #1987, #7452, #6849, #6888, #4876, #3839, #2516, #7414, #785, #5685, #4957, #1912, #1235, #6170, #6130, #639, #3091, #5528, #1277, #4915, #1868, #4315 ),
 .UNSPECIFIED., .F., .F.,
 ( 4, 2, 2, 2, 2, 2, 2, 2, 2, 2, 2, 2, 2, 2, 2, 2, 2, 2, 2, 2, 2, 2, 2, 2, 4 ),
 ( 0.000000000000000000, 0.002511627799209755017, 0.003767441698814711672, 0.005023255598419669628, 0.007534883397629582938, 0.01004651119683949712, 0.01130232509644451058, 0.01255813899604952405, 0.01506976679525946078, 0.01632558069486442914, 0.01758139459446940098, 0.02009302239367936893, 0.02134883629328435117, 0.02260465019288934035, 0.02386046409249432260, 0.02511627799209930484, 0.02762790579130921381, 0.03013953359051911585, 0.03139534749012407033, 0.03265116138972902482, 0.03516278918893894073, 0.03641860308854381889, 0.03767441698814869705, 0.03893023088775358215, 0.04018604478735846031 ),
 .UNSPECIFIED. ) ;
#774=CARTESIAN_POINT ( 'NONE',  ( 398.6828372460798846, -12.50000000000000000, -14.73776325548316812 ) ) ;
#775=EDGE_LOOP ( 'NONE', ( #3337, #854 ) ) ;
#785=CARTESIAN_POINT ( 'NONE',  ( 366.7510386178572048, 17.65558712887547443, 9.400222409301415283 ) ) ;
#797=CARTESIAN_POINT ( 'NONE',  ( 340.0000000000000000, 12.50000000000000000, 15.61249499599599488 ) ) ;
#798=DIRECTION ( 'NONE',  ( -0.7071067811865479058, 0.000000000000000000, 0.7071067811865472397 ) ) ;
#802=VECTOR ( 'NONE', #5540, 1000.000000000000000 ) ;
#820=EDGE_CURVE ( 'NONE', #1377, #6439, #6344, .T. ) ;
#827=ORIENTED_EDGE ( 'NONE', *, *, #6507, .T. ) ;
#828=VECTOR ( 'NONE', #1297, 1000.000000000000000 ) ;
#837=ORIENTED_EDGE ( 'NONE', *, *, #6507, .F. ) ;
#840=DIRECTION ( 'NONE',  ( 0.000000000000000000, 0.000000000000000000, 1.000000000000000000 ) ) ;
#851=ORIENTED_EDGE ( 'NONE', *, *, #7776, .T. ) ;
#854=ORIENTED_EDGE ( 'NONE', *, *, #6480, .F. ) ;
#859=CARTESIAN_POINT ( 'NONE',  ( 190.0000000000000000, 3.061616997868383043E-15, -25.00000000000000000 ) ) ;
#863=ORIENTED_EDGE ( 'NONE', *, *, #7066, .F. ) ;
#866=DIRECTION ( 'NONE',  ( -1.000000000000000000, -0.000000000000000000, -0.000000000000000000 ) ) ;
#880=CARTESIAN_POINT ( 'NONE',  ( 340.0000000000000000, 0.000000000000000000, 0.000000000000000000 ) ) ;
#888=CARTESIAN_POINT ( 'NONE',  ( 340.0000000000000000, -12.50000000000000355, 21.65063509461096558 ) ) ;
#891=DIRECTION ( 'NONE',  ( -1.000000000000000000, -0.000000000000000000, -0.000000000000000000 ) ) ;
#894=EDGE_LOOP ( 'NONE', ( #2327, #6080 ) ) ;
#900=EDGE_CURVE ( 'NONE', #968, #1507, #4611, .T. ) ;
#920=DIRECTION ( 'NONE',  ( -0.000000000000000000, -1.000000000000000000, -0.000000000000000000 ) ) ;
#925=CARTESIAN_POINT ( 'NONE',  ( 375.0000000000000000, 25.00000000000000000, 12.50000000000000711 ) ) ;
#926=DIRECTION ( 'NONE',  ( 1.000000000000000000, 0.000000000000000000, 0.000000000000000000 ) ) ;
#927=CARTESIAN_POINT ( 'NONE',  ( 377.9033602712955826, 15.87504132268115242, 12.16528391369894990 ) ) ;
#939=DIRECTION ( 'NONE',  ( -1.000000000000000000, 0.000000000000000000, -0.000000000000000000 ) ) ;
#943=ORIENTED_EDGE ( 'NONE', *, *, #2332, .F. ) ;
#950=CIRCLE ( 'NONE', #3261, 15.00000000000000000 ) ;
#956=DIRECTION ( 'NONE',  ( 0.000000000000000000, 0.000000000000000000, -1.000000000000000000 ) ) ;
#958=ADVANCED_BREP_SHAPE_REPRESENTATION ( '', ( #6795, #5785 ), #536 ) ;
#968=VERTEX_POINT ( 'NONE', #5711 ) ;
#974=CARTESIAN_POINT ( 'NONE',  ( 385.7934419064004032, 18.97653311414304511, 6.355249004872655760 ) ) ;
#982=VERTEX_POINT ( 'NONE', #1489 ) ;
#985=FACE_OUTER_BOUND ( 'NONE', #1432, .T. ) ;
#1078=DIRECTION ( 'NONE',  ( 0.000000000000000000, 0.000000000000000000, 1.000000000000000000 ) ) ;
#1086=AXIS2_PLACEMENT_3D ( 'NONE', #2762, #5149, #2035 ) ;
#1089=CARTESIAN_POINT ( 'NONE',  ( 175.0000000000000000, 0.000000000000000000, 0.000000000000000000 ) ) ;
#1099=FACE_OUTER_BOUND ( 'NONE', #3873, .T. ) ;
#1105=CARTESIAN_POINT ( 'NONE',  ( 325.0000000000000000, 0.000000000000000000, 0.000000000000000000 ) ) ;
#1109=AXIS2_PLACEMENT_3D ( 'NONE', #690, #3750, #5633 ) ;
#1116=CARTESIAN_POINT ( 'NONE',  ( 370.8902687158968092, -16.13982617348050752, -11.81224944216114459 ) ) ;
#1120=CIRCLE ( 'NONE', #2531, 25.00000000000000000 ) ;
#1130=CARTESIAN_POINT ( 'NONE',  ( 379.1097312841034181, 16.13982617348050752, -11.81224944216114459 ) ) ;
#1132=CIRCLE ( 'NONE', #3448, 12.50000000000000355 ) ;
#1139=DIRECTION ( 'NONE',  ( -1.000000000000000000, 0.000000000000000000, -0.000000000000000000 ) ) ;
#1147=ORIENTED_EDGE ( 'NONE', *, *, #5859, .F. ) ;
#1150=DIRECTION ( 'NONE',  ( 0.000000000000000000, 0.000000000000000000, -1.000000000000000000 ) ) ;
#1160=CARTESIAN_POINT ( 'NONE',  ( 364.4192847381275442, -18.85911174686545166, -6.667915149371354211 ) ) ;
#1162=DIRECTION ( 'NONE',  ( -1.000000000000000000, -0.000000000000000000, -0.000000000000000000 ) ) ;
#1165=EDGE_CURVE ( 'NONE', #6439, #6276, #4254, .T. ) ;
#1168=CARTESIAN_POINT ( 'NONE',  ( 383.5435001242829571, -17.79554561421092984, 9.133253117746194860 ) ) ;
#1185=CARTESIAN_POINT ( 'NONE',  ( 0.000000000000000000, 0.000000000000000000, 0.000000000000000000 ) ) ;
#1193=CARTESIAN_POINT ( 'NONE',  ( 373.3215647054732358, -15.68173745365923288, 12.41480524315420197 ) ) ;
#1197=VECTOR ( 'NONE', #2659, 1000.000000000000000 ) ;
#1199=AXIS2_PLACEMENT_3D ( 'NONE', #5771, #270, #2717 ) ;
#1200=EDGE_LOOP ( 'NONE', ( #7084, #6403, #6235, #2079 ) ) ;
#1234=VERTEX_POINT ( 'NONE', #2416 ) ;
#1235=CARTESIAN_POINT ( 'NONE',  ( 369.3855057752896300, 16.57606561041850313, 11.19744344920339962 ) ) ;
#1237=CARTESIAN_POINT ( 'NONE',  ( 370.5191279495746244, -16.23886410922228052, 11.67632056536055707 ) ) ;
#1244=ORIENTED_EDGE ( 'NONE', *, *, #5410, .F. ) ;
#1247=CARTESIAN_POINT ( 'NONE',  ( 387.4981577384509706, -19.99884858813039301, -0.8730781214943976742 ) ) ;
#1248=CARTESIAN_POINT ( 'NONE',  ( 325.0000000000000000, 0.000000000000000000, 0.000000000000000000 ) ) ;
#1257=FACE_BOUND ( 'NONE', #7583, .T. ) ;
#1264=ORIENTED_EDGE ( 'NONE', *, *, #1299, .F. ) ;
#1277=CARTESIAN_POINT ( 'NONE',  ( 373.3129592716863385, 15.69785030319133945, 12.39275847443047773 ) ) ;
#1278=ORIENTED_EDGE ( 'NONE', *, *, #900, .T. ) ;
#1279=CARTESIAN_POINT ( 'NONE',  ( 368.6712260976869970, -16.83573837738345702, -10.80867071580873784 ) ) ;
#1285=ORIENTED_EDGE ( 'NONE', *, *, #2144, .F. ) ;
#1297=DIRECTION ( 'NONE',  ( -1.000000000000000000, -0.000000000000000000, -0.000000000000000000 ) ) ;
#1299=EDGE_CURVE ( 'NONE', #2585, #136, #3706, .T. ) ;
#1312=CARTESIAN_POINT ( 'NONE',  ( 369.3970366575052822, 16.57206429410149795, -11.20336317960804884 ) ) ;
#1316=( NAMED_UNIT ( * ) SI_UNIT ( $, .STERADIAN. ) SOLID_ANGLE_UNIT ( ) );
#1320=VERTEX_POINT ( 'NONE', #5817 ) ;
#1323=CARTESIAN_POINT ( 'NONE',  ( 386.1955684391606951, -19.21001202690979781, 5.620007094727602848 ) ) ;
#1330=DIRECTION ( 'NONE',  ( -0.000000000000000000, 0.000000000000000000, 1.000000000000000000 ) ) ;
#1331=CARTESIAN_POINT ( 'NONE',  ( 325.0000000000000000, -12.50000000000000000, -21.65063509461096558 ) ) ;
#1339=CARTESIAN_POINT ( 'NONE',  ( 375.0000000000000000, 25.00000000000000000, 12.50000000000000711 ) ) ;
#1342=VECTOR ( 'NONE', #6596, 1000.000000000000000 ) ;
#1344=ORIENTED_EDGE ( 'NONE', *, *, #480, .T. ) ;
#1348=ORIENTED_EDGE ( 'NONE', *, *, #2046, .F. ) ;
#1354=FACE_BOUND ( 'NONE', #119, .T. ) ;
#1359=ORIENTED_EDGE ( 'NONE', *, *, #190, .T. ) ;
#1362=CARTESIAN_POINT ( 'NONE',  ( 6.249999999999977796, 0.000000000000000000, 25.00000000000000000 ) ) ;
#1369=DIRECTION ( 'NONE',  ( -1.000000000000000000, 0.000000000000000000, -0.000000000000000000 ) ) ;
#1376=DIRECTION ( 'NONE',  ( 0.7071067811865517916, 0.000000000000000000, -0.7071067811865431318 ) ) ;
#1377=VERTEX_POINT ( 'NONE', #797 ) ;
#1387=CARTESIAN_POINT ( 'NONE',  ( 365.1198422076048473, 18.47484582708395706, -7.667708004838452496 ) ) ;
#1398=CARTESIAN_POINT ( 'NONE',  ( 398.6828372460798846, -12.50000000000000000, 14.73776325548316812 ) ) ;
#1404=CARTESIAN_POINT ( 'NONE',  ( 386.8066430167523890, -19.57388548866421019, -4.126530372600788255 ) ) ;
#1405=CARTESIAN_POINT ( 'NONE',  ( 375.0000000000000000, 12.50000000000000000, 3.061616997868383043E-15 ) ) ;
#1422=ORIENTED_EDGE ( 'NONE', *, *, #5037, .F. ) ;
#1432=EDGE_LOOP ( 'NONE', ( #837, #5779, #6835 ) ) ;
#1437=CARTESIAN_POINT ( 'NONE',  ( 400.0000000000000000, 12.50000000000000000, -12.95183384698871620 ) ) ;
#1457=DIRECTION ( 'NONE',  ( 1.000000000000000000, 0.000000000000000000, 0.000000000000000000 ) ) ;
#1470=FACE_OUTER_BOUND ( 'NONE', #5331, .T. ) ;
#1489=CARTESIAN_POINT ( 'NONE',  ( 325.0000000000000000, 12.50000000000000000, -21.65063509461096913 ) ) ;
#1499=CARTESIAN_POINT ( 'NONE',  ( 400.0000000000000000, -12.50000000000000000, 12.95183384698871620 ) ) ;
#1505=CIRCLE ( 'NONE', #4956, 25.00000000000000000 ) ;
#1507=VERTEX_POINT ( 'NONE', #3834 ) ;
#1512=DIRECTION ( 'NONE',  ( 0.000000000000000000, 0.000000000000000000, -1.000000000000000000 ) ) ;
#1529=AXIS2_PLACEMENT_3D ( 'NONE', #2288, #1796, #1678 ) ;
#1535=LINE ( 'NONE', #6428, #7102 ) ;
#1539=ORIENTED_EDGE ( 'NONE', *, *, #68, .F. ) ;
#1548=CARTESIAN_POINT ( 'NONE',  ( 375.0000000000000000, 25.00000000000000000, 3.061616997868383043E-15 ) ) ;
#1555=LINE ( 'NONE', #2850, #5881 ) ;
#1569=CARTESIAN_POINT ( 'NONE',  ( 385.1211727163475302, 18.60519396204907139, 7.346513279853128964 ) ) ;
#1573=CARTESIAN_POINT ( 'NONE',  ( 375.0000000000000000, -12.50000000000000355, 3.061616997868383043E-15 ) ) ;
#1578=VERTEX_POINT ( 'NONE', #4508 ) ;
#1587=EDGE_CURVE ( 'NONE', #6561, #1, #5067, .T. ) ;
#1673=DIRECTION ( 'NONE',  ( -1.000000000000000000, -0.000000000000000000, -0.000000000000000000 ) ) ;
#1678=DIRECTION ( 'NONE',  ( 0.000000000000000000, 0.000000000000000000, 1.000000000000000000 ) ) ;
#1680=DIRECTION ( 'NONE',  ( -1.000000000000000000, -0.000000000000000000, -0.000000000000000000 ) ) ;
#1691=CARTESIAN_POINT ( 'NONE',  ( 0.000000000000000000, 0.000000000000000000, 0.000000000000000000 ) ) ;
#1692=CARTESIAN_POINT ( 'NONE',  ( 379.4971731025975146, 16.24331487217730796, -11.67016537472322746 ) ) ;
#1715=CARTESIAN_POINT ( 'NONE',  ( 370.9025538143762901, -16.13667248250984798, 11.81655595281366899 ) ) ;
#1719=VECTOR ( 'NONE', #6239, 1000.000000000000000 ) ;
#1726=LINE ( 'NONE', #6029, #7669 ) ;
#1730=CARTESIAN_POINT ( 'NONE',  ( 383.5484565773660393, 17.79791451299709948, -9.128686039268288255 ) ) ;
#1740=ORIENTED_EDGE ( 'NONE', *, *, #3722, .T. ) ;
#1748=DIRECTION ( 'NONE',  ( 0.000000000000000000, 0.000000000000000000, -1.000000000000000000 ) ) ;
#1749=FACE_OUTER_BOUND ( 'NONE', #3812, .T. ) ;
#1756=ORIENTED_EDGE ( 'NONE', *, *, #2718, .T. ) ;
#1757=CARTESIAN_POINT ( 'NONE',  ( 362.8306064000756805, -19.79494591053120445, -2.886379146895018177 ) ) ;
#1766=EDGE_CURVE ( 'NONE', #3409, #4567, #1781, .T. ) ;
#1776=PRODUCT_CONTEXT ( 'NONE', #3012, 'mechanical' ) ;
#1779=AXIS2_PLACEMENT_3D ( 'NONE', #1248, #650, #726 ) ;
#1781=LINE ( 'NONE', #4780, #1342 ) ;
#1783=AXIS2_PLACEMENT_3D ( 'NONE', #3355, #939, #4592 ) ;
#1796=DIRECTION ( 'NONE',  ( -1.000000000000000000, -0.000000000000000000, -0.000000000000000000 ) ) ;
#1798=CARTESIAN_POINT ( 'NONE',  ( 367.3584912393716309, -17.37175308249308969, 9.924386979199645964 ) ) ;
#1804=ORIENTED_EDGE ( 'NONE', *, *, #6562, .F. ) ;
#1807=DIRECTION ( 'NONE',  ( 1.000000000000000000, 0.000000000000000000, 0.000000000000000000 ) ) ;
#1812=CARTESIAN_POINT ( 'NONE',  ( 376.6960688664906911, 15.69870025322426699, -12.39168528959425331 ) ) ;
#1827=CARTESIAN_POINT ( 'NONE',  ( 365.6323756216988272, 18.20590005533475875, -8.286065263872075093 ) ) ;
#1829=CARTESIAN_POINT ( 'NONE',  ( 371.6902873359033492, -15.95485291322333588, 12.06092292949322520 ) ) ;
#1846=CARTESIAN_POINT ( 'NONE',  ( 398.0000000000001137, -12.50000000000000000, 15.61249499599599488 ) ) ;
#1850=CARTESIAN_POINT ( 'NONE',  ( 400.0000000000000000, -12.50000000000000000, 12.95183384698871620 ) ) ;
#1851=CARTESIAN_POINT ( 'NONE',  ( 375.0000000000000000, -15.61249499599599488, 12.50000000000000711 ) ) ;
#1868=CARTESIAN_POINT ( 'NONE',  ( 374.5752787360723914, 15.61249499599598956, 12.50000000000000533 ) ) ;
#1870=CARTESIAN_POINT ( 'NONE',  ( 362.9351699716481221, -19.73070161726337446, -3.295910870315892804 ) ) ;
#1907=ORIENTED_EDGE ( 'NONE', *, *, #7596, .T. ) ;
#1912=CARTESIAN_POINT ( 'NONE',  ( 368.6844851971966932, 16.83062759343247805, 10.81672997705310557 ) ) ;
#1920=ORIENTED_EDGE ( 'NONE', *, *, #6916, .F. ) ;
#1922=DIRECTION ( 'NONE',  ( 1.000000000000000000, 0.000000000000000000, 0.000000000000000000 ) ) ;
#1923=CARTESIAN_POINT ( 'NONE',  ( 384.8801577923950390, -18.47484582708395706, -7.667708004838452496 ) ) ;
#1945=CARTESIAN_POINT ( 'NONE',  ( 374.1480243754402863, 15.61249499599599311, -12.50000000000000000 ) ) ;
#1949=CARTESIAN_POINT ( 'NONE',  ( 340.0000000000000000, 12.50000000000000000, -21.65063509461096913 ) ) ;
#1965=AXIS2_PLACEMENT_3D ( 'NONE', #517, #3598, #6046 ) ;
#1966=FACE_OUTER_BOUND ( 'NONE', #4644, .T. ) ;
#1974=ADVANCED_FACE ( 'NONE', ( #6194, #6830 ), #5594, .T. ) ;
#1980=EDGE_CURVE ( 'NONE', #3124, #4547, #5637, .T. ) ;
#1987=CARTESIAN_POINT ( 'NONE',  ( 362.9348919987150452, 19.73086988975742528, 3.295070860296623216 ) ) ;
#1991=DIRECTION ( 'NONE',  ( 1.000000000000000000, 0.000000000000000000, 0.000000000000000000 ) ) ;
#1997=CIRCLE ( 'NONE', #7393, 25.00000000000000000 ) ;
#2001=DIRECTION ( 'NONE',  ( 0.000000000000000000, -1.000000000000000000, 0.000000000000000000 ) ) ;
#2002=CARTESIAN_POINT ( 'NONE',  ( 386.1839732711879378, -19.20325634068194631, -5.642343897998047808 ) ) ;
#2014=AXIS2_PLACEMENT_3D ( 'NONE', #2605, #2001, #4442 ) ;
#2015=ORIENTED_EDGE ( 'NONE', *, *, #7776, .F. ) ;
#2019=AXIS2_PLACEMENT_3D ( 'NONE', #1405, #920, #6299 ) ;
#2030=DIRECTION ( 'NONE',  ( 0.000000000000000000, 0.000000000000000000, -1.000000000000000000 ) ) ;
#2035=DIRECTION ( 'NONE',  ( 0.000000000000000000, 0.000000000000000000, 1.000000000000000000 ) ) ;
#2036=EDGE_CURVE ( 'NONE', #982, #6900, #771, .T. ) ;
#2038=ORIENTED_EDGE ( 'NONE', *, *, #4734, .F. ) ;
#2044=ADVANCED_FACE ( 'NONE', ( #6386, #6990 ), #3301, .T. ) ;
#2045=CARTESIAN_POINT ( 'NONE',  ( 398.6828372460798846, 12.50000000000000000, -14.73776325548316812 ) ) ;
#2046=EDGE_CURVE ( 'NONE', #7248, #7215, #7873, .T. ) ;
#2051=CARTESIAN_POINT ( 'NONE',  ( 340.0000000000000000, 12.50000000000000000, 0.000000000000000000 ) ) ;
#2057=VERTEX_POINT ( 'NONE', #4012 ) ;
#2059=FACE_OUTER_BOUND ( 'NONE', #4711, .T. ) ;
#2066=CARTESIAN_POINT ( 'NONE',  ( 190.0000000000000000, 0.000000000000000000, 0.000000000000000000 ) ) ;
#2074=VECTOR ( 'NONE', #3182, 1000.000000000000000 ) ;
#2079=ORIENTED_EDGE ( 'NONE', *, *, #6505, .T. ) ;
#2080=DIRECTION ( 'NONE',  ( 0.000000000000000000, 0.000000000000000000, -1.000000000000000000 ) ) ;
#2110=DIRECTION ( 'NONE',  ( 0.000000000000000000, -1.000000000000000000, 0.000000000000000000 ) ) ;
#2111=CYLINDRICAL_SURFACE ( 'NONE', #6451, 15.00000000000000000 ) ;
#2114=ORIENTED_EDGE ( 'NONE', *, *, #5066, .F. ) ;
#2127=PRODUCT ( 'Rod', 'Rod', '', ( #1776 ) ) ;
#2128=DIRECTION ( 'NONE',  ( 0.000000000000000000, 0.000000000000000000, -1.000000000000000000 ) ) ;
#2144=EDGE_CURVE ( 'NONE', #322, #3264, #1535, .T. ) ;
#2148=VECTOR ( 'NONE', #3681, 1000.000000000000000 ) ;
#2176=CARTESIAN_POINT ( 'NONE',  ( 384.1017607431604688, 18.07018020958731697, 8.577132482464245200 ) ) ;
#2194=AXIS2_PLACEMENT_3D ( 'NONE', #2066, #5727, #4029 ) ;
#2211=EDGE_LOOP ( 'NONE', ( #863, #4082, #6575, #3883 ) ) ;
#2219=CARTESIAN_POINT ( 'NONE',  ( 398.6828372460798846, 12.50000000000000000, 14.73776325548316812 ) ) ;
#2249=CARTESIAN_POINT ( 'NONE',  ( 190.0000000000000000, 0.000000000000000000, 0.000000000000000000 ) ) ;
#2264=CARTESIAN_POINT ( 'NONE',  ( 376.6784352945268779, 15.68173745365923288, 12.41480524315420197 ) ) ;
#2275=CIRCLE ( 'NONE', #3295, 12.50000000000000355 ) ;
#2277=ORIENTED_EDGE ( 'NONE', *, *, #2573, .F. ) ;
#2281=AXIS2_PLACEMENT_3D ( 'NONE', #7706, #5167, #2128 ) ;
#2288=CARTESIAN_POINT ( 'NONE',  ( 398.0000000000001137, 0.000000000000000000, 0.000000000000000000 ) ) ;
#2290=CARTESIAN_POINT ( 'NONE',  ( 374.1528078369840387, -15.61249499599599844, 12.50000000000001066 ) ) ;
#2302=DIRECTION ( 'NONE',  ( 0.000000000000000000, 0.000000000000000000, -1.000000000000000000 ) ) ;
#2307=CARTESIAN_POINT ( 'NONE',  ( 387.4992068747945950, 19.99950429724430023, 0.4454306286988182761 ) ) ;
#2321=VERTEX_POINT ( 'NONE', #1846 ) ;
#2327=ORIENTED_EDGE ( 'NONE', *, *, #1299, .T. ) ;
#2329=DIRECTION ( 'NONE',  ( 0.000000000000000000, 0.000000000000000000, 1.000000000000000000 ) ) ;
#2332=EDGE_CURVE ( 'NONE', #1578, #3245, #5160, .T. ) ;
#2339=CARTESIAN_POINT ( 'NONE',  ( 386.8189259714962986, 19.58130419088990948, -4.090982884146981746 ) ) ;
#2343=CARTESIAN_POINT ( 'NONE',  ( 0.000000000000000000, 0.000000000000000000, 15.00000000000000000 ) ) ;
#2351=DIRECTION ( 'NONE',  ( 1.000000000000000000, 0.000000000000000000, 0.000000000000000000 ) ) ;
#2356=DIRECTION ( 'NONE',  ( -1.000000000000000000, -0.000000000000000000, -0.000000000000000000 ) ) ;
#2357=ORIENTED_EDGE ( 'NONE', *, *, #2144, .T. ) ;
#2363=CARTESIAN_POINT ( 'NONE',  ( 362.5007931252055187, -19.99950429724430023, 0.4454306286988182761 ) ) ;
#2369=AXIS2_PLACEMENT_3D ( 'NONE', #5979, #6057, #4205 ) ;
#2370=CARTESIAN_POINT ( 'NONE',  ( 379.1121327631079225, -16.14034269873396710, 11.81156333678811876 ) ) ;
#2406=DIRECTION ( 'NONE',  ( 1.000000000000000000, 0.000000000000000000, 0.000000000000000000 ) ) ;
#2413=CARTESIAN_POINT ( 'NONE',  ( 377.0997413288390021, -15.74791738283697740, 12.32940567573685087 ) ) ;
#2416=CARTESIAN_POINT ( 'NONE',  ( 398.0000000000001137, 12.50000000000000000, 15.61249499599599488 ) ) ;
#2418=CARTESIAN_POINT ( 'NONE',  ( 375.0000000000000000, 15.61249499599599488, -12.50000000000000000 ) ) ;
#2421=SHAPE_DEFINITION_REPRESENTATION ( #4492, #4527 ) ;
#2427=LINE ( 'NONE', #5593, #828 ) ;
#2441=CARTESIAN_POINT ( 'NONE',  ( 362.4991219212881788, 20.00054879841449562, 0.3963588355767777571 ) ) ;
#2445=( LENGTH_UNIT ( ) NAMED_UNIT ( * ) SI_UNIT ( .MILLI., .METRE. ) );
#2458=CARTESIAN_POINT ( 'NONE',  ( 387.4765783011941380, 19.98534102192048323, 0.8725863811532602599 ) ) ;
#2469=CARTESIAN_POINT ( 'NONE',  ( 340.0000000000000000, 12.50000000000000000, -15.61249499599599488 ) ) ;
#2476=CARTESIAN_POINT ( 'NONE',  ( 368.6894672773787534, 16.82862359362766469, -10.81999899256329911 ) ) ;
#2478=CARTESIAN_POINT ( 'NONE',  ( 365.1180127946531115, -18.47584224143657039, 7.665216593424116986 ) ) ;
#2488=ORIENTED_EDGE ( 'NONE', *, *, #820, .T. ) ;
#2492=CARTESIAN_POINT ( 'NONE',  ( 387.3337822858457002, -19.89643035834168927, 2.074044983930025232 ) ) ;
#2514=AXIS2_PLACEMENT_3D ( 'NONE', #1548, #2110, #1512 ) ;
#2516=CARTESIAN_POINT ( 'NONE',  ( 365.6127344411505646, 18.21073727249144625, 8.292169370763099678 ) ) ;
#2531=AXIS2_PLACEMENT_3D ( 'NONE', #880, #281, #840 ) ;
#2538=PLANE ( 'NONE',  #3044 ) ;
#2554=CIRCLE ( 'NONE', #7036, 20.00000000000000000 ) ;
#2558=CARTESIAN_POINT ( 'NONE',  ( 362.9438371151090905, 19.72539574521466932, -3.327763323014857555 ) ) ;
#2559=EDGE_LOOP ( 'NONE', ( #2357, #5062, #1264, #65, #5031, #2488, #6544, #1359, #5456, #3854 ) ) ;
#2560=CARTESIAN_POINT ( 'NONE',  ( 375.0000000000000000, 25.00000000000000000, 3.061616997868383043E-15 ) ) ;
#2568=CARTESIAN_POINT ( 'NONE',  ( 377.9017428551080116, -15.87479745381989815, -12.16559770555248754 ) ) ;
#2573=EDGE_CURVE ( 'NONE', #2057, #6240, #950, .T. ) ;
#2576=CARTESIAN_POINT ( 'NONE',  ( 400.0000000000000000, -12.50000000000000000, 25.00000000000000000 ) ) ;
#2582=PRODUCT_DEFINITION_FORMATION_WITH_SPECIFIED_SOURCE ( 'ANY', '', #2127, .NOT_KNOWN. ) ;
#2585=VERTEX_POINT ( 'NONE', #3293 ) ;
#2594=DIRECTION ( 'NONE',  ( 0.000000000000000000, 0.000000000000000000, 1.000000000000000000 ) ) ;
#2605=CARTESIAN_POINT ( 'NONE',  ( 375.0000000000000000, 25.00000000000000000, 3.061616997868383043E-15 ) ) ;
#2606=CARTESIAN_POINT ( 'NONE',  ( 383.2551259162264614, -17.65381669312412427, -9.419798908014916705 ) ) ;
#2607=ORIENTED_EDGE ( 'NONE', *, *, #7682, .T. ) ;
#2613=FACE_OUTER_BOUND ( 'NONE', #894, .T. ) ;
#2643=VERTEX_POINT ( 'NONE', #4006 ) ;
#2651=CARTESIAN_POINT ( 'NONE',  ( 325.0000000000000000, 3.061616997868383043E-15, -25.00000000000000000 ) ) ;
#2659=DIRECTION ( 'NONE',  ( 0.000000000000000000, -1.000000000000000000, 0.000000000000000000 ) ) ;
#2676=CARTESIAN_POINT ( 'NONE',  ( 175.0000000000000000, 0.000000000000000000, 0.000000000000000000 ) ) ;
#2685=EDGE_CURVE ( 'NONE', #136, #2585, #6461, .T. ) ;
#2690=CARTESIAN_POINT ( 'NONE',  ( 340.0000000000000000, -12.50000000000000355, 0.000000000000000000 ) ) ;
#2698=DIRECTION ( 'NONE',  ( 0.000000000000000000, 0.000000000000000000, -1.000000000000000000 ) ) ;
#2714=CYLINDRICAL_SURFACE ( 'NONE', #2194, 20.00000000000000000 ) ;
#2717=DIRECTION ( 'NONE',  ( 0.000000000000000000, 0.000000000000000000, 1.000000000000000000 ) ) ;
#2718=EDGE_CURVE ( 'NONE', #1234, #3264, #6598, .T. ) ;
#2720=CARTESIAN_POINT ( 'NONE',  ( 190.0000000000000000, 0.000000000000000000, 0.000000000000000000 ) ) ;
#2762=CARTESIAN_POINT ( 'NONE',  ( 340.0000000000000000, 0.000000000000000000, 0.000000000000000000 ) ) ;
#2767=LINE ( 'NONE', #5199, #70 ) ;
#2774=ORIENTED_EDGE ( 'NONE', *, *, #1980, .T. ) ;
#2794=VECTOR ( 'NONE', #1162, 1000.000000000000000 ) ;
#2810=CARTESIAN_POINT ( 'NONE',  ( 6.249999999999977796, 0.000000000000000000, 0.000000000000000000 ) ) ;
#2816=VECTOR ( 'NONE', #599, 1000.000000000000000 ) ;
#2836=CONICAL_SURFACE ( 'NONE', #12, 15.00000000000000000, 0.7853981633974479459 ) ;
#2844=CIRCLE ( 'NONE', #1529, 20.00000000000000000 ) ;
#2850=CARTESIAN_POINT ( 'NONE',  ( 0.000000000000000000, 2.296212748401299411E-15, 18.75000000000009948 ) ) ;
#2865=CARTESIAN_POINT ( 'NONE',  ( 379.0974461856235393, 16.13667248250984798, 11.81655595281366899 ) ) ;
#2870=CARTESIAN_POINT ( 'NONE',  ( 340.0000000000000000, 25.00000000000000000, 0.000000000000000000 ) ) ;
#2893=DIRECTION ( 'NONE',  ( -1.000000000000000000, -0.000000000000000000, -0.000000000000000000 ) ) ;
#2899=AXIS2_PLACEMENT_3D ( 'NONE', #5284, #1680, #956 ) ;
#2906=AXIS2_PLACEMENT_3D ( 'NONE', #2810, #6452, #5329 ) ;
#2907=CARTESIAN_POINT ( 'NONE',  ( 380.5932282495298864, 16.58082631454064781, 11.18611842067925011 ) ) ;
#2932=CARTESIAN_POINT ( 'NONE',  ( 375.0000000000000000, -15.61249499599599488, 12.50000000000000711 ) ) ;
#2945=ADVANCED_FACE ( 'NONE', ( #3994 ), #5078, .T. ) ;
#2951=CARTESIAN_POINT ( 'NONE',  ( 385.7933296785779476, 18.97948036624223533, -6.318259067610828339 ) ) ;
#2971=EDGE_CURVE ( 'NONE', #1320, #3444, #4538, .T. ) ;
#2972=CARTESIAN_POINT ( 'NONE',  ( 372.8893025888656894, -15.74939801616919866, -12.32751675873151598 ) ) ;
#2992=LINE ( 'NONE', #4658, #7157 ) ;
#2996=EDGE_LOOP ( 'NONE', ( #5743, #7692, #228, #6782, #5229, #7208, #3505, #7006 ) ) ;
#3009=CARTESIAN_POINT ( 'NONE',  ( 369.3727881274253946, -16.58005916595991280, -11.19168395254304471 ) ) ;
#3012=APPLICATION_CONTEXT ( 'automotive_design' ) ;
#3014=AXIS2_PLACEMENT_3D ( 'NONE', #7263, #2406, #2329 ) ;
#3020=CARTESIAN_POINT ( 'NONE',  ( 385.8076615439897523, -18.98451973267744464, 6.332666029034883515 ) ) ;
#3044=AXIS2_PLACEMENT_3D ( 'NONE', #2576, #5052, #768 ) ;
#3054=CARTESIAN_POINT ( 'NONE',  ( 190.0000000000000000, 1.836970198721029589E-15, -15.00000000000000000 ) ) ;
#3064=CARTESIAN_POINT ( 'NONE',  ( 379.4812749451934337, -16.23897639391231706, -11.67616422689687639 ) ) ;
#3068=CARTESIAN_POINT ( 'NONE',  ( 386.3591492015264635, 19.30709367143974831, -5.233317247790644444 ) ) ;
#3075=DIRECTION ( 'NONE',  ( -1.000000000000000000, -0.000000000000000000, -0.000000000000000000 ) ) ;
#3091=CARTESIAN_POINT ( 'NONE',  ( 372.0849291719837311, 15.87720460852527715, 12.16246356757440950 ) ) ;
#3093=CARTESIAN_POINT ( 'NONE',  ( 363.3331590693758812, -19.48969576164946105, 4.506197270647787967 ) ) ;
#3101=CARTESIAN_POINT ( 'NONE',  ( 383.2489613821426246, -17.65558712887547443, 9.400222409301415283 ) ) ;
#3124=VERTEX_POINT ( 'NONE', #557 ) ;
#3126=FACE_OUTER_BOUND ( 'NONE', #7078, .T. ) ;
#3128=CARTESIAN_POINT ( 'NONE',  ( 366.7494411481458769, -17.65634310857833356, -9.398786704980601314 ) ) ;
#3129=ORIENTED_EDGE ( 'NONE', *, *, #2718, .F. ) ;
#3137=CARTESIAN_POINT ( 'NONE',  ( 377.9150708280164395, -15.87720460852527715, 12.16246356757440950 ) ) ;
#3138=CARTESIAN_POINT ( 'NONE',  ( 384.3676243783012296, -18.20590005533475875, -8.286065263872075093 ) ) ;
#3155=CARTESIAN_POINT ( 'NONE',  ( 340.0000000000000000, -12.50000000000000355, 0.000000000000000000 ) ) ;
#3163=CARTESIAN_POINT ( 'NONE',  ( 363.8160267288120622, 19.20325634068194631, -5.642343897998047808 ) ) ;
#3177=LINE ( 'NONE', #2690, #4703 ) ;
#3182=DIRECTION ( 'NONE',  ( -1.000000000000000000, -0.000000000000000000, -0.000000000000000000 ) ) ;
#3193=SHAPE_REPRESENTATION_RELATIONSHIP ( 'NONE' , 'NONE' ,  #4527, #958 ) ;
#3204=CARTESIAN_POINT ( 'NONE',  ( 363.3366216376737157, 19.48763309926589216, -4.514690562563614229 ) ) ;
#3205=EDGE_LOOP ( 'NONE', ( #3428, #827, #7787 ) ) ;
#3208=FACE_OUTER_BOUND ( 'NONE', #3365, .T. ) ;
#3214=FACE_OUTER_BOUND ( 'NONE', #4399, .T. ) ;
#3215=CARTESIAN_POINT ( 'NONE',  ( 379.0967594850577598, -16.13643827696138189, -11.81688677216110861 ) ) ;
#3219=EDGE_CURVE ( 'NONE', #7215, #7248, #4415, .T. ) ;
#3222=DIRECTION ( 'NONE',  ( 1.000000000000000000, 0.000000000000000000, 0.000000000000000000 ) ) ;
#3224=DIRECTION ( 'NONE',  ( 0.000000000000000000, -1.000000000000000000, 0.000000000000000000 ) ) ;
#3225=CARTESIAN_POINT ( 'NONE',  ( 190.0000000000000000, 12.50000000000000000, -21.65063509461096913 ) ) ;
#3237=CARTESIAN_POINT ( 'NONE',  ( 366.7448740837735954, 17.65381669312412427, -9.419798908014916705 ) ) ;
#3245=VERTEX_POINT ( 'NONE', #7813 ) ;
#3258=CARTESIAN_POINT ( 'NONE',  ( 375.0000000000000000, 25.00000000000000000, -12.50000000000000000 ) ) ;
#3261=AXIS2_PLACEMENT_3D ( 'NONE', #5125, #7062, #4525 ) ;
#3264=VERTEX_POINT ( 'NONE', #3729 ) ;
#3270=LINE ( 'NONE', #7678, #4912 ) ;
#3288=B_SPLINE_CURVE_WITH_KNOTS ( 'NONE', 3,
 ( #5950, #1398, #4815, #1850 ),
 .UNSPECIFIED., .F., .F.,
 ( 4, 4 ),
 ( 0.000000000000000000, 0.003328530869593411285 ),
 .UNSPECIFIED. ) ;
#3289=ORIENTED_EDGE ( 'NONE', *, *, #6169, .T. ) ;
#3290=LINE ( 'NONE', #3929, #4964 ) ;
#3293=CARTESIAN_POINT ( 'NONE',  ( 400.0000000000000000, 12.50000000000000000, 12.95183384698871620 ) ) ;
#3295=AXIS2_PLACEMENT_3D ( 'NONE', #1573, #4698, #261 ) ;
#3297=CIRCLE ( 'NONE', #2281, 25.00000000000000000 ) ;
#3301=PLANE ( 'NONE',  #3397 ) ;
#3304=PRODUCT_DEFINITION ( 'UNKNOWN', '', #2582, #4225 ) ;
#3337=ORIENTED_EDGE ( 'NONE', *, *, #6505, .F. ) ;
#3355=CARTESIAN_POINT ( 'NONE',  ( 400.0000000000000000, 20.00000000000000000, 0.000000000000000000 ) ) ;
#3365=EDGE_LOOP ( 'NONE', ( #7473, #4955 ) ) ;
#3372=B_SPLINE_CURVE_WITH_KNOTS ( 'NONE', 3,
 ( #7544, #2045, #4487, #1437 ),
 .UNSPECIFIED., .F., .F.,
 ( 4, 4 ),
 ( 0.000000000000000000, 0.003328530869593411285 ),
 .UNSPECIFIED. ) ;
#3373=ORIENTED_EDGE ( 'NONE', *, *, #820, .F. ) ;
#3378=CARTESIAN_POINT ( 'NONE',  ( 379.4808720504254325, 16.23886410922228052, 11.67632056536055707 ) ) ;
#3382=CARTESIAN_POINT ( 'NONE',  ( 399.3518360003419048, 12.50000000000000000, 13.85262921941843750 ) ) ;
#3387=DIRECTION ( 'NONE',  ( 1.000000000000000000, 0.000000000000000000, 0.000000000000000000 ) ) ;
#3397=AXIS2_PLACEMENT_3D ( 'NONE', #4096, #3938, #2698 ) ;
#3403=ORIENTED_EDGE ( 'NONE', *, *, #5117, .F. ) ;
#3409=VERTEX_POINT ( 'NONE', #290 ) ;
#3419=DIRECTION ( 'NONE',  ( -1.000000000000000000, -0.000000000000000000, -0.000000000000000000 ) ) ;
#3423=CARTESIAN_POINT ( 'NONE',  ( 386.1818624296773805, 19.20198692117305583, 5.648001166226691794 ) ) ;
#3428=ORIENTED_EDGE ( 'NONE', *, *, #3666, .F. ) ;
#3430=PLANE ( 'NONE',  #7795 ) ;
#3434=CIRCLE ( 'NONE', #5354, 25.00000000000000000 ) ;
#3439=DIRECTION ( 'NONE',  ( 0.000000000000000000, 0.000000000000000000, 1.000000000000000000 ) ) ;
#3444=VERTEX_POINT ( 'NONE', #4097 ) ;
#3448=AXIS2_PLACEMENT_3D ( 'NONE', #583, #6192, #3714 ) ;
#3455=ORIENTED_EDGE ( 'NONE', *, *, #6480, .T. ) ;
#3502=DIRECTION ( 'NONE',  ( 0.000000000000000000, 0.000000000000000000, -1.000000000000000000 ) ) ;
#3505=ORIENTED_EDGE ( 'NONE', *, *, #4734, .T. ) ;
#3507=EDGE_CURVE ( 'NONE', #968, #3409, #388, .T. ) ;
#3545=VECTOR ( 'NONE', #5677, 1000.000000000000000 ) ;
#3568=CARTESIAN_POINT ( 'NONE',  ( 363.8181375703225626, -19.20198692117305583, 5.648001166226691794 ) ) ;
#3569=ORIENTED_EDGE ( 'NONE', *, *, #6409, .T. ) ;
#3584=CARTESIAN_POINT ( 'NONE',  ( 375.4248592744880852, 15.61249499599599666, -12.50000000000000000 ) ) ;
#3590=CARTESIAN_POINT ( 'NONE',  ( 375.0000000000000000, 25.00000000000000000, 3.061616997868383043E-15 ) ) ;
#3598=DIRECTION ( 'NONE',  ( -1.000000000000000000, -0.000000000000000000, -0.000000000000000000 ) ) ;
#3606=CARTESIAN_POINT ( 'NONE',  ( 365.6048426980225372, -18.21476284106545052, -8.283543559714008353 ) ) ;
#3616=CARTESIAN_POINT ( 'NONE',  ( 380.6144942247103131, -16.57606561041850313, 11.19744344920339962 ) ) ;
#3645=AXIS2_PLACEMENT_3D ( 'NONE', #6608, #1673, #6566 ) ;
#3646=CARTESIAN_POINT ( 'NONE',  ( 365.0969724145188025, -18.48453940650270866, -7.670107965951052265 ) ) ;
#3664=CARTESIAN_POINT ( 'NONE',  ( 383.2505588518543505, 17.65634310857833356, -9.398786704980601314 ) ) ;
#3666=EDGE_CURVE ( 'NONE', #6766, #2057, #2767, .T. ) ;
#3675=EDGE_CURVE ( 'NONE', #4927, #1, #596, .T. ) ;
#3676=EDGE_CURVE ( 'NONE', #3245, #1578, #6736, .T. ) ;
#3681=DIRECTION ( 'NONE',  ( 0.000000000000000000, -1.000000000000000000, 0.000000000000000000 ) ) ;
#3685=VECTOR ( 'NONE', #5599, 1000.000000000000000 ) ;
#3691=CARTESIAN_POINT ( 'NONE',  ( 364.8773838277618324, 18.60597098153023055, -7.344632615169738088 ) ) ;
#3693=CARTESIAN_POINT ( 'NONE',  ( 364.2066703214222230, -18.97948036624223533, -6.318259067610828339 ) ) ;
#3704=CARTESIAN_POINT ( 'NONE',  ( 387.5008780787119349, -20.00054879841449562, 0.3963588355767777571 ) ) ;
#3706=LINE ( 'NONE', #4292, #802 ) ;
#3713=CARTESIAN_POINT ( 'NONE',  ( 325.0000000000000000, 0.000000000000000000, 0.000000000000000000 ) ) ;
#3714=DIRECTION ( 'NONE',  ( 0.000000000000000000, 0.000000000000000000, 1.000000000000000000 ) ) ;
#3719=ADVANCED_FACE ( 'NONE', ( #5932 ), #7736, .F. ) ;
#3722=EDGE_CURVE ( 'NONE', #4474, #4547, #3749, .T. ) ;
#3729=CARTESIAN_POINT ( 'NONE',  ( 398.0000000000001137, 12.50000000000000000, -15.61249499599599488 ) ) ;
#3733=CARTESIAN_POINT ( 'NONE',  ( 362.8398061413552114, 19.78928940797825931, -2.924464941254242056 ) ) ;
#3743=CARTESIAN_POINT ( 'NONE',  ( 384.8984063742112767, -18.48201531705921141, 7.676572043282099855 ) ) ;
#3744=CARTESIAN_POINT ( 'NONE',  ( 387.3963605620842827, -19.93536271250352598, 1.660494579713906127 ) ) ;
#3745=DIRECTION ( 'NONE',  ( -0.000000000000000000, -1.000000000000000000, -0.000000000000000000 ) ) ;
#3749=B_SPLINE_CURVE_WITH_KNOTS ( 'NONE', 3,
 ( #2932, #2290, #1193, #4278, #1829, #1715, #1237, #7301, #4240, #29, #5530, #1798, #6690, #4160, #6054, #2478, #4878, #66, #3568, #3093, #7260, #7219, #6616, #4798, #5451, #6774, #2363, #5405, #6173, #1757, #1870, #4201, #4918, #6729, #6657, #3693, #1160, #3646, #3606, #560, #3128, #6017, #4317, #1279, #3009, #6132, #1116, #6095, #523, #2972, #7888, #5491, #7850, #7377 ),
 .UNSPECIFIED., .F., .F.,
 ( 4, 2, 2, 2, 2, 2, 2, 2, 2, 2, 2, 2, 2, 2, 2, 2, 2, 2, 2, 2, 2, 2, 2, 2, 2, 2, 4 ),
 ( 0.04018604478735846031, 0.04269101871805709714, 0.04394350568340633229, 0.04519599264875557437, 0.04644847961410480952, 0.04770096657945405161, 0.05020594051015265374, 0.05145842747550190277, 0.05271091444085115874, 0.05521588837154975393, 0.05646837533689905153, 0.05772086230224834913, 0.05897334926759764673, 0.06022583623294694433, 0.06273081016364553952, 0.06398329712899483712, 0.06523578409434413472, 0.06648827105969341844, 0.06774075802504271604, 0.07024573195574131124, 0.07149821892109066435, 0.07275070588644001746, 0.07525567981713872368, 0.07650816678248806291, 0.07776065374783742989, 0.07901314071318678300, 0.08026562767853613611 ),
 .UNSPECIFIED. ) ;
#3750=DIRECTION ( 'NONE',  ( -1.000000000000000000, 0.000000000000000000, -0.000000000000000000 ) ) ;
#3751=CARTESIAN_POINT ( 'NONE',  ( 340.0000000000000000, 0.000000000000000000, 0.000000000000000000 ) ) ;
#3758=LINE ( 'NONE', #1339, #2148 ) ;
#3765=ADVANCED_FACE ( 'NONE', ( #1470 ), #7491, .F. ) ;
#3787=DIRECTION ( 'NONE',  ( 0.000000000000000000, 0.000000000000000000, 1.000000000000000000 ) ) ;
#3801=CARTESIAN_POINT ( 'NONE',  ( 365.9011734668954432, 18.06872101906905215, -8.580138959277956445 ) ) ;
#3812=EDGE_LOOP ( 'NONE', ( #5393, #943, #485, #3846 ) ) ;
#3827=CARTESIAN_POINT ( 'NONE',  ( 398.0000000000001137, -12.50000000000000000, -15.61249499599599488 ) ) ;
#3834=CARTESIAN_POINT ( 'NONE',  ( 375.0000000000000000, 12.50000000000000000, 12.50000000000000711 ) ) ;
#3839=CARTESIAN_POINT ( 'NONE',  ( 365.1015936257888939, 18.48201531705921141, 7.676572043282099855 ) ) ;
#3844=DIRECTION ( 'NONE',  ( -1.000000000000000000, -0.000000000000000000, -0.000000000000000000 ) ) ;
#3846=ORIENTED_EDGE ( 'NONE', *, *, #3675, .F. ) ;
#3854=ORIENTED_EDGE ( 'NONE', *, *, #5719, .T. ) ;
#3860=CARTESIAN_POINT ( 'NONE',  ( 375.0000000000000000, -15.61249499599599488, -12.50000000000000000 ) ) ;
#3865=CARTESIAN_POINT ( 'NONE',  ( 400.0000000000000000, -12.50000000000000000, -12.95183384698871798 ) ) ;
#3873=EDGE_LOOP ( 'NONE', ( #5847, #5882, #3373, #3962 ) ) ;
#3880=DIRECTION ( 'NONE',  ( 0.000000000000000000, 0.000000000000000000, 1.000000000000000000 ) ) ;
#3883=ORIENTED_EDGE ( 'NONE', *, *, #7596, .F. ) ;
#3904=CARTESIAN_POINT ( 'NONE',  ( 0.000000000000000000, 0.000000000000000000, -18.75000000000009948 ) ) ;
#3914=ORIENTED_EDGE ( 'NONE', *, *, #7296, .T. ) ;
#3929=CARTESIAN_POINT ( 'NONE',  ( 325.0000000000000000, -12.50000000000000000, 25.00000000000000000 ) ) ;
#3938=DIRECTION ( 'NONE',  ( 0.000000000000000000, -1.000000000000000000, -0.000000000000000000 ) ) ;
#3939=MECHANICAL_DESIGN_GEOMETRIC_PRESENTATION_REPRESENTATION('',(#6768),#5239);
#3962=ORIENTED_EDGE ( 'NONE', *, *, #7765, .T. ) ;
#3968=ADVANCED_FACE ( 'NONE', ( #432 ), #7049, .F. ) ;
#3994=FACE_OUTER_BOUND ( 'NONE', #6246, .T. ) ;
#4006=CARTESIAN_POINT ( 'NONE',  ( 325.0000000000000000, 0.000000000000000000, 25.00000000000000000 ) ) ;
#4012=CARTESIAN_POINT ( 'NONE',  ( 175.0000000000000000, 1.836970198721029589E-15, -15.00000000000000000 ) ) ;
#4029=DIRECTION ( 'NONE',  ( 0.000000000000000000, 0.000000000000000000, 1.000000000000000000 ) ) ;
#4082=ORIENTED_EDGE ( 'NONE', *, *, #6640, .F. ) ;
#4090=EDGE_CURVE ( 'NONE', #6561, #982, #1997, .T. ) ;
#4091=ORIENTED_EDGE ( 'NONE', *, *, #4491, .T. ) ;
#4096=CARTESIAN_POINT ( 'NONE',  ( 400.0000000000000000, 12.50000000000000000, 25.00000000000000000 ) ) ;
#4097=CARTESIAN_POINT ( 'NONE',  ( 340.0000000000000000, -12.50000000000000355, 15.61249499599599311 ) ) ;
#4110=CARTESIAN_POINT ( 'NONE',  ( 0.000000000000000000, 0.000000000000000000, 0.000000000000000000 ) ) ;
#4111=ORIENTED_EDGE ( 'NONE', *, *, #4236, .T. ) ;
#4120=CARTESIAN_POINT ( 'NONE',  ( 190.0000000000000000, -12.50000000000000000, 21.65063509461096913 ) ) ;
#4124=DIRECTION ( 'NONE',  ( 0.000000000000000000, 0.000000000000000000, 1.000000000000000000 ) ) ;
#4153=ORIENTED_EDGE ( 'NONE', *, *, #6796, .T. ) ;
#4156=VECTOR ( 'NONE', #5669, 1000.000000000000000 ) ;
#4160=CARTESIAN_POINT ( 'NONE',  ( 365.8982392568397017, -18.07018020958731697, 8.577132482464245200 ) ) ;
#4173=CARTESIAN_POINT ( 'NONE',  ( 387.5015236343236893, 20.00095227047670576, -0.8223324121160918709 ) ) ;
#4186=DIRECTION ( 'NONE',  ( 0.000000000000000000, 0.000000000000000000, 1.000000000000000000 ) ) ;
#4201=CARTESIAN_POINT ( 'NONE',  ( 363.1810740285039287, -19.58130419088990948, -4.090982884146981746 ) ) ;
#4205=DIRECTION ( 'NONE',  ( 0.000000000000000000, 0.000000000000000000, 1.000000000000000000 ) ) ;
#4206=EDGE_LOOP ( 'NONE', ( #451, #5261, #1740, #6197 ) ) ;
#4211=EDGE_CURVE ( 'NONE', #6240, #7248, #5642, .T. ) ;
#4225=PRODUCT_DEFINITION_CONTEXT ( 'detailed design', #6434, 'design' ) ;
#4230=FACE_OUTER_BOUND ( 'NONE', #2211, .T. ) ;
#4236=EDGE_CURVE ( 'NONE', #4609, #3444, #700, .T. ) ;
#4240=CARTESIAN_POINT ( 'NONE',  ( 369.4067717504701704, -16.58082631454064781, 11.18611842067925011 ) ) ;
#4241=ORIENTED_EDGE ( 'NONE', *, *, #5859, .T. ) ;
#4250=CARTESIAN_POINT ( 'NONE',  ( 325.0000000000000000, 0.000000000000000000, 0.000000000000000000 ) ) ;
#4253=CARTESIAN_POINT ( 'NONE',  ( 340.0000000000000000, 12.50000000000000000, 21.65063509461096913 ) ) ;
#4254=LINE ( 'NONE', #614, #2074 ) ;
#4268=ORIENTED_EDGE ( 'NONE', *, *, #7101, .F. ) ;
#4278=CARTESIAN_POINT ( 'NONE',  ( 372.0966397287041900, -15.87504132268115242, 12.16528391369894990 ) ) ;
#4279=ORIENTED_EDGE ( 'NONE', *, *, #7066, .T. ) ;
#4286=EDGE_CURVE ( 'NONE', #3124, #5409, #2275, .T. ) ;
#4290=CARTESIAN_POINT ( 'NONE',  ( 385.1226161722381107, -18.60597098153023055, -7.344632615169738088 ) ) ;
#4292=CARTESIAN_POINT ( 'NONE',  ( 400.0000000000000000, 12.50000000000000000, 25.00000000000000000 ) ) ;
#4315=CARTESIAN_POINT ( 'NONE',  ( 375.0000000000000000, 15.61249499599599488, 12.50000000000000711 ) ) ;
#4317=CARTESIAN_POINT ( 'NONE',  ( 367.6834352059303797, -17.23925164521633846, -10.14275924251023220 ) ) ;
#4324=ORIENTED_EDGE ( 'NONE', *, *, #5969, .T. ) ;
#4326=CARTESIAN_POINT ( 'NONE',  ( 387.0651080012848411, -19.73086988975742528, 3.295070860296623216 ) ) ;
#4336=CARTESIAN_POINT ( 'NONE',  ( 340.0000000000000000, 25.00000000000000000, 0.000000000000000000 ) ) ;
#4365=CARTESIAN_POINT ( 'NONE',  ( 386.8183406672370666, -19.58094920198549360, 4.092816503359988367 ) ) ;
#4387=CARTESIAN_POINT ( 'NONE',  ( 362.5200448844577750, 19.98745133777255134, 0.8232361438305751955 ) ) ;
#4399=EDGE_LOOP ( 'NONE', ( #851, #1278, #3455, #7343 ) ) ;
#4408=AXIS2_PLACEMENT_3D ( 'NONE', #2720, #6490, #3880 ) ;
#4409=AXIS2_PLACEMENT_3D ( 'NONE', #5298, #891, #5132 ) ;
#4415=CIRCLE ( 'NONE', #196, 15.00000000000000000 ) ;
#4425=CARTESIAN_POINT ( 'NONE',  ( 378.3097126640965939, 15.95485291322333588, 12.06092292949322520 ) ) ;
#4429=CARTESIAN_POINT ( 'NONE',  ( 370.9032405149421834, 16.13643827696138189, -11.81688677216110861 ) ) ;
#4431=DIRECTION ( 'NONE',  ( 0.000000000000000000, -1.000000000000000000, 0.000000000000000000 ) ) ;
#4434=LINE ( 'NONE', #6892, #105 ) ;
#4440=ORIENTED_EDGE ( 'NONE', *, *, #718, .F. ) ;
#4442=DIRECTION ( 'NONE',  ( 0.000000000000000000, 0.000000000000000000, -1.000000000000000000 ) ) ;
#4448=ADVANCED_FACE ( 'NONE', ( #2613 ), #7356, .F. ) ;
#4474=VERTEX_POINT ( 'NONE', #1851 ) ;
#4485=ADVANCED_FACE ( 'NONE', ( #1257, #1966 ), #2538, .T. ) ;
#4487=CARTESIAN_POINT ( 'NONE',  ( 399.3518360003419048, 12.50000000000000000, -13.85262921941844816 ) ) ;
#4491=EDGE_CURVE ( 'NONE', #5961, #6561, #1505, .T. ) ;
#4492=PRODUCT_DEFINITION_SHAPE ( 'NONE', 'NONE',  #3304 ) ;
#4500=VERTEX_POINT ( 'NONE', #6152 ) ;
#4507=ADVANCED_FACE ( 'NONE', ( #6912 ), #5590, .F. ) ;
#4508=CARTESIAN_POINT ( 'NONE',  ( 0.000000000000000000, 0.000000000000000000, -18.75000000000009948 ) ) ;
#4515=DIRECTION ( 'NONE',  ( 0.000000000000000000, 0.000000000000000000, -1.000000000000000000 ) ) ;
#4525=DIRECTION ( 'NONE',  ( 0.000000000000000000, 0.000000000000000000, 1.000000000000000000 ) ) ;
#4527=SHAPE_REPRESENTATION ( 'Rod', ( #5785 ), #536 ) ;
#4538=CIRCLE ( 'NONE', #1086, 20.00000000000000000 ) ;
#4547=VERTEX_POINT ( 'NONE', #3860 ) ;
#4567=VERTEX_POINT ( 'NONE', #6305 ) ;
#4592=DIRECTION ( 'NONE',  ( -0.000000000000000000, 0.000000000000000000, 1.000000000000000000 ) ) ;
#4604=DIRECTION ( 'NONE',  ( 1.000000000000000000, 0.000000000000000000, 0.000000000000000000 ) ) ;
#4609=VERTEX_POINT ( 'NONE', #888 ) ;
#4611=LINE ( 'NONE', #925, #7866 ) ;
#4613=CARTESIAN_POINT ( 'NONE',  ( 384.3729953227158944, 18.20868245435311295, 8.279865652961362343 ) ) ;
#4621=EDGE_LOOP ( 'NONE', ( #4440, #1756, #1285, #7545 ) ) ;
#4627=ORIENTED_EDGE ( 'NONE', *, *, #3219, .F. ) ;
#4644=EDGE_LOOP ( 'NONE', ( #1344, #3914, #3289, #4279, #6221, #6920, #4324, #2114, #2607, #4111 ) ) ;
#4645=EDGE_CURVE ( 'NONE', #1, #4927, #3297, .T. ) ;
#4652=CARTESIAN_POINT ( 'NONE',  ( 387.3259369069866693, 19.89156578813670251, 2.119594365942482739 ) ) ;
#4658=CARTESIAN_POINT ( 'NONE',  ( 340.0000000000000000, 12.50000000000000000, 0.000000000000000000 ) ) ;
#4680=DIRECTION ( 'NONE',  ( 0.000000000000000000, 0.000000000000000000, 1.000000000000000000 ) ) ;
#4690=CARTESIAN_POINT ( 'NONE',  ( 325.0000000000000000, 12.50000000000000000, 21.65063509461096913 ) ) ;
#4698=DIRECTION ( 'NONE',  ( 0.000000000000000000, 1.000000000000000000, 0.000000000000000000 ) ) ;
#4700=CYLINDRICAL_SURFACE ( 'NONE', #5432, 12.50000000000000355 ) ;
#4703=VECTOR ( 'NONE', #5623, 1000.000000000000000 ) ;
#4711=EDGE_LOOP ( 'NONE', ( #5023, #7689, #3569, #670, #4091, #6571 ) ) ;
#4724=FACE_OUTER_BOUND ( 'NONE', #5701, .T. ) ;
#4734=EDGE_CURVE ( 'NONE', #2643, #4927, #6665, .T. ) ;
#4736=CARTESIAN_POINT ( 'NONE',  ( 387.1693935999242058, 19.79494591053120445, -2.886379146895018177 ) ) ;
#4746=ORIENTED_EDGE ( 'NONE', *, *, #4645, .T. ) ;
#4752=CARTESIAN_POINT ( 'NONE',  ( 400.0000000000000000, 12.50000000000000000, -12.95183384698871620 ) ) ;
#4770=CARTESIAN_POINT ( 'NONE',  ( 384.9030275854814818, 18.48453940650270866, -7.670107965951052265 ) ) ;
#4780=CARTESIAN_POINT ( 'NONE',  ( 375.0000000000000000, 25.00000000000000000, -12.50000000000000000 ) ) ;
#4798=CARTESIAN_POINT ( 'NONE',  ( 362.6740630930135580, -19.89156578813670251, 2.119594365942482739 ) ) ;
#4803=ADVANCED_FACE ( 'NONE', ( #5460 ), #5604, .T. ) ;
#4807=CARTESIAN_POINT ( 'NONE',  ( 375.0000000000000000, -15.61249499599599488, 12.50000000000000711 ) ) ;
#4815=CARTESIAN_POINT ( 'NONE',  ( 399.3518360003419048, -12.50000000000000000, 13.85262921941844816 ) ) ;
#4834=VERTEX_POINT ( 'NONE', #7826 ) ;
#4876=CARTESIAN_POINT ( 'NONE',  ( 364.1923384560104182, 18.98451973267744464, 6.332666029034883515 ) ) ;
#4878=CARTESIAN_POINT ( 'NONE',  ( 364.8788272836525266, -18.60519396204907139, 7.346513279853128964 ) ) ;
#4892=CARTESIAN_POINT ( 'NONE',  ( 385.5807152618725127, 18.85911174686545166, -6.667915149371354211 ) ) ;
#4912=VECTOR ( 'NONE', #3387, 1000.000000000000000 ) ;
#4915=CARTESIAN_POINT ( 'NONE',  ( 374.1490196022552936, 15.63011725355127624, 12.47807683047398619 ) ) ;
#4918=CARTESIAN_POINT ( 'NONE',  ( 363.3225212018339789, -19.49607926063143282, -4.478210459206754201 ) ) ;
#4927=VERTEX_POINT ( 'NONE', #1362 ) ;
#4932=CARTESIAN_POINT ( 'NONE',  ( 387.1681567566444642, -19.79418587323000267, 2.891333466711802469 ) ) ;
#4936=AXIS2_PLACEMENT_3D ( 'NONE', #2560, #4431, #2030 ) ;
#4955=ORIENTED_EDGE ( 'NONE', *, *, #3676, .T. ) ;
#4956=AXIS2_PLACEMENT_3D ( 'NONE', #3713, #3222, #7397 ) ;
#4957=CARTESIAN_POINT ( 'NONE',  ( 367.6909075080810112, 17.23604965026853009, 10.14822696828370319 ) ) ;
#4964=VECTOR ( 'NONE', #2080, 1000.000000000000000 ) ;
#4968=AXIS2_PLACEMENT_3D ( 'NONE', #153, #1991, #4515 ) ;
#4971=EDGE_CURVE ( 'NONE', #4547, #4474, #7901, .T. ) ;
#4973=CARTESIAN_POINT ( 'NONE',  ( 382.6434889735085108, -17.37246880845878039, -9.923319895790875478 ) ) ;
#5000=CARTESIAN_POINT ( 'NONE',  ( 362.8318432433553085, 19.79418587323000267, 2.891333466711802469 ) ) ;
#5018=CARTESIAN_POINT ( 'NONE',  ( 190.0000000000000000, 0.000000000000000000, 0.000000000000000000 ) ) ;
#5023=ORIENTED_EDGE ( 'NONE', *, *, #190, .F. ) ;
#5030=CARTESIAN_POINT ( 'NONE',  ( 362.6662177141545271, 19.89643035834168927, 2.074044983930025232 ) ) ;
#5031=ORIENTED_EDGE ( 'NONE', *, *, #718, .T. ) ;
#5037=EDGE_CURVE ( 'NONE', #6276, #2643, #3434, .T. ) ;
#5052=DIRECTION ( 'NONE',  ( 0.000000000000000000, 1.000000000000000000, 0.000000000000000000 ) ) ;
#5062=ORIENTED_EDGE ( 'NONE', *, *, #6562, .T. ) ;
#5063=CARTESIAN_POINT ( 'NONE',  ( 190.0000000000000000, 0.000000000000000000, 15.00000000000000000 ) ) ;
#5066=EDGE_CURVE ( 'NONE', #4500, #5961, #3290, .T. ) ;
#5067=LINE ( 'NONE', #859, #1719 ) ;
#5076=EDGE_LOOP ( 'NONE', ( #2277, #4153, #7731, #7576 ) ) ;
#5078=CYLINDRICAL_SURFACE ( 'NONE', #4408, 25.00000000000000000 ) ;
#5084=ORIENTED_EDGE ( 'NONE', *, *, #4211, .T. ) ;
#5088=CONICAL_SURFACE ( 'NONE', #5207, 18.75000000000009948, 0.7853981633974421728 ) ;
#5099=VECTOR ( 'NONE', #13, 1000.000000000000000 ) ;
#5117=EDGE_CURVE ( 'NONE', #1320, #7097, #3177, .T. ) ;
#5125=CARTESIAN_POINT ( 'NONE',  ( 175.0000000000000000, 0.000000000000000000, 0.000000000000000000 ) ) ;
#5132=DIRECTION ( 'NONE',  ( 0.000000000000000000, 0.000000000000000000, 1.000000000000000000 ) ) ;
#5133=EDGE_CURVE ( 'NONE', #7097, #4609, #1120, .T. ) ;
#5138=DIRECTION ( 'NONE',  ( 0.000000000000000000, 0.000000000000000000, -1.000000000000000000 ) ) ;
#5141=ORIENTED_EDGE ( 'NONE', *, *, #7166, .F. ) ;
#5143=FACE_OUTER_BOUND ( 'NONE', #4621, .T. ) ;
#5149=DIRECTION ( 'NONE',  ( -1.000000000000000000, -0.000000000000000000, -0.000000000000000000 ) ) ;
#5160=CIRCLE ( 'NONE', #5694, 18.75000000000009948 ) ;
#5167=DIRECTION ( 'NONE',  ( 1.000000000000000000, 0.000000000000000000, 0.000000000000000000 ) ) ;
#5176=CARTESIAN_POINT ( 'NONE',  ( 399.3518360003419048, -12.50000000000000000, -13.85262921941843750 ) ) ;
#5184=EDGE_LOOP ( 'NONE', ( #7218, #7087, #3403, #7299 ) ) ;
#5186=EDGE_LOOP ( 'NONE', ( #5304, #7685, #7172, #4268 ) ) ;
#5189=ADVANCED_FACE ( 'NONE', ( #3214 ), #159, .F. ) ;
#5191=CARTESIAN_POINT ( 'NONE',  ( 190.0000000000000000, 0.000000000000000000, 0.000000000000000000 ) ) ;
#5199=CARTESIAN_POINT ( 'NONE',  ( 175.0000000000000000, 1.836970198721029589E-15, -15.00000000000000000 ) ) ;
#5207=AXIS2_PLACEMENT_3D ( 'NONE', #1185, #4604, #7653 ) ;
#5216=ADVANCED_FACE ( 'NONE', ( #1749 ), #5088, .T. ) ;
#5229=ORIENTED_EDGE ( 'NONE', *, *, #7682, .F. ) ;
#5239=( GEOMETRIC_REPRESENTATION_CONTEXT ( 3 ) GLOBAL_UNCERTAINTY_ASSIGNED_CONTEXT ( ( #7372 ) ) GLOBAL_UNIT_ASSIGNED_CONTEXT ( ( #2445, #7379, #1316 ) ) REPRESENTATION_CONTEXT ( 'NONE', 'WORKASPACE' ) );
#5258=CARTESIAN_POINT ( 'NONE',  ( 387.1586741829164566, 19.78835583758980832, 2.930536303278098664 ) ) ;
#5261=ORIENTED_EDGE ( 'NONE', *, *, #5410, .T. ) ;
#5271=UNCERTAINTY_MEASURE_WITH_UNIT (LENGTH_MEASURE( 1.000000000000000082E-05 ), #94, 'distance_accuracy_value', 'NONE');
#5278=ORIENTED_EDGE ( 'NONE', *, *, #4971, .F. ) ;
#5284=CARTESIAN_POINT ( 'NONE',  ( 0.000000000000000000, 0.000000000000000000, 0.000000000000000000 ) ) ;
#5289=DIRECTION ( 'NONE',  ( 1.000000000000000000, 0.000000000000000000, 0.000000000000000000 ) ) ;
#5298=CARTESIAN_POINT ( 'NONE',  ( 0.000000000000000000, 0.000000000000000000, 0.000000000000000000 ) ) ;
#5299=CARTESIAN_POINT ( 'NONE',  ( 375.8471921630161887, 15.61249499599599844, 12.50000000000001066 ) ) ;
#5304=ORIENTED_EDGE ( 'NONE', *, *, #3676, .F. ) ;
#5316=EDGE_LOOP ( 'NONE', ( #2015, #63 ) ) ;
#5318=LINE ( 'NONE', #7770, #7855 ) ;
#5329=DIRECTION ( 'NONE',  ( 0.000000000000000000, 0.000000000000000000, -1.000000000000000000 ) ) ;
#5331=EDGE_LOOP ( 'NONE', ( #1244, #4241, #2774, #7140 ) ) ;
#5344=CARTESIAN_POINT ( 'NONE',  ( 381.3043660624298923, 16.83403191367835561, 10.80131548116625417 ) ) ;
#5353=ORIENTED_EDGE ( 'NONE', *, *, #1165, .F. ) ;
#5354=AXIS2_PLACEMENT_3D ( 'NONE', #4250, #1922, #532 ) ;
#5357=VECTOR ( 'NONE', #1376, 1000.000000000000114 ) ;
#5372=CONICAL_SURFACE ( 'NONE', #7037, 15.00000000000000000, 0.7853981633974479459 ) ;
#5382=CARTESIAN_POINT ( 'NONE',  ( 175.0000000000000000, 0.000000000000000000, 15.00000000000000000 ) ) ;
#5388=B_SPLINE_CURVE_WITH_KNOTS ( 'NONE', 3,
 ( #3865, #5176, #774, #3827 ),
 .UNSPECIFIED., .F., .F.,
 ( 4, 4 ),
 ( 1.734723475976807094E-18, 0.003328530869593415188 ),
 .UNSPECIFIED. ) ;
#5390=DIRECTION ( 'NONE',  ( -0.000000000000000000, 0.000000000000000000, 1.000000000000000000 ) ) ;
#5393=ORIENTED_EDGE ( 'NONE', *, *, #7487, .F. ) ;
#5405=CARTESIAN_POINT ( 'NONE',  ( 362.4984763656763107, -20.00095227047670576, -0.8223324121160918709 ) ) ;
#5407=CARTESIAN_POINT ( 'NONE',  ( 190.0000000000000000, 0.000000000000000000, 0.000000000000000000 ) ) ;
#5409=VERTEX_POINT ( 'NONE', #6717 ) ;
#5410=EDGE_CURVE ( 'NONE', #5409, #4474, #3758, .T. ) ;
#5432=AXIS2_PLACEMENT_3D ( 'NONE', #3590, #5878, #382 ) ;
#5439=FACE_OUTER_BOUND ( 'NONE', #2996, .T. ) ;
#5443=CARTESIAN_POINT ( 'NONE',  ( 0.000000000000000000, 0.000000000000000000, 0.000000000000000000 ) ) ;
#5451=CARTESIAN_POINT ( 'NONE',  ( 362.6101369827622420, -19.93132096080314497, 1.708129828930195826 ) ) ;
#5456=ORIENTED_EDGE ( 'NONE', *, *, #2036, .T. ) ;
#5460=FACE_OUTER_BOUND ( 'NONE', #5186, .T. ) ;
#5491=CARTESIAN_POINT ( 'NONE',  ( 374.1492488978694837, -15.62998136526340076, -12.47825053757332370 ) ) ;
#5507=CARTESIAN_POINT ( 'NONE',  ( 382.6349272670254322, 17.37719324208310923, -9.905392396107414399 ) ) ;
#5510=LINE ( 'NONE', #6753, #5099 ) ;
#5516=VERTEX_POINT ( 'NONE', #1499 ) ;
#5522=ORIENTED_EDGE ( 'NONE', *, *, #5962, .T. ) ;
#5528=CARTESIAN_POINT ( 'NONE',  ( 372.9002586711609410, 15.74791738283697740, 12.32940567573685087 ) ) ;
#5530=CARTESIAN_POINT ( 'NONE',  ( 368.3509586464906533, -16.96668907523693548, 10.59241602951089867 ) ) ;
#5536=CARTESIAN_POINT ( 'NONE',  ( 384.3872655588493785, -18.21073727249144625, 8.292169370763099678 ) ) ;
#5538=CARTESIAN_POINT ( 'NONE',  ( 387.4799551155421682, -19.98745133777255134, 0.8232361438305751955 ) ) ;
#5540=DIRECTION ( 'NONE',  ( 0.000000000000000000, 0.000000000000000000, -1.000000000000000000 ) ) ;
#5550=( NAMED_UNIT ( * ) SI_UNIT ( $, .STERADIAN. ) SOLID_ANGLE_UNIT ( ) );
#5565=CARTESIAN_POINT ( 'NONE',  ( 364.2021130961084623, 18.97902931052027142, -6.348195341973490891 ) ) ;
#5580=ORIENTED_EDGE ( 'NONE', *, *, #480, .F. ) ;
#5590=PLANE ( 'NONE',  #7401 ) ;
#5593=CARTESIAN_POINT ( 'NONE',  ( 190.0000000000000000, 12.50000000000000000, 15.61249499599599488 ) ) ;
#5594=CYLINDRICAL_SURFACE ( 'NONE', #704, 20.00000000000000000 ) ;
#5599=DIRECTION ( 'NONE',  ( 0.000000000000000000, 0.000000000000000000, -1.000000000000000000 ) ) ;
#5604=CONICAL_SURFACE ( 'NONE', #5990, 18.75000000000009948, 0.7853981633974421728 ) ;
#5615=CONICAL_SURFACE ( 'NONE', #739, 20.00000000000000000, 0.7853981633974578269 ) ;
#5623=DIRECTION ( 'NONE',  ( 0.000000000000000000, 0.000000000000000000, -1.000000000000000000 ) ) ;
#5633=DIRECTION ( 'NONE',  ( -0.000000000000000000, 0.000000000000000000, 1.000000000000000000 ) ) ;
#5635=CIRCLE ( 'NONE', #1779, 25.00000000000000000 ) ;
#5637=LINE ( 'NONE', #3258, #1197 ) ;
#5642=LINE ( 'NONE', #5063, #3545 ) ;
#5648=CARTESIAN_POINT ( 'NONE',  ( 363.1933569832476678, 19.57388548866421019, -4.126530372600788255 ) ) ;
#5653=PLANE ( 'NONE',  #4968 ) ;
#5660=CARTESIAN_POINT ( 'NONE',  ( 380.6029633424947747, -16.57206429410149795, -11.20336317960804884 ) ) ;
#5664=ADVANCED_FACE ( 'NONE', ( #2059 ), #3430, .T. ) ;
#5669=DIRECTION ( 'NONE',  ( 1.000000000000000000, 0.000000000000000000, 0.000000000000000000 ) ) ;
#5673=B_SPLINE_CURVE_WITH_KNOTS ( 'NONE', 3,
 ( #462, #3382, #2219, #7711 ),
 .UNSPECIFIED., .F., .F.,
 ( 4, 4 ),
 ( 0.000000000000000000, 0.003328530869593415188 ),
 .UNSPECIFIED. ) ;
#5674=CARTESIAN_POINT ( 'NONE',  ( 340.0000000000000000, -12.50000000000000355, -21.65063509461096558 ) ) ;
#5677=DIRECTION ( 'NONE',  ( -1.000000000000000000, -0.000000000000000000, -0.000000000000000000 ) ) ;
#5685=CARTESIAN_POINT ( 'NONE',  ( 367.3680131217492999, 17.37589182433591972, 9.907690019304302709 ) ) ;
#5694=AXIS2_PLACEMENT_3D ( 'NONE', #1691, #6031, #3502 ) ;
#5701=EDGE_LOOP ( 'NONE', ( #5141, #173, #1804, #3129 ) ) ;
#5711=CARTESIAN_POINT ( 'NONE',  ( 375.0000000000000000, 15.61249499599599488, 12.50000000000000711 ) ) ;
#5719=EDGE_CURVE ( 'NONE', #6900, #322, #2992, .T. ) ;
#5727=DIRECTION ( 'NONE',  ( -1.000000000000000000, -0.000000000000000000, -0.000000000000000000 ) ) ;
#5743=ORIENTED_EDGE ( 'NONE', *, *, #1587, .F. ) ;
#5771=CARTESIAN_POINT ( 'NONE',  ( 175.0000000000000000, 0.000000000000000000, 0.000000000000000000 ) ) ;
#5779=ORIENTED_EDGE ( 'NONE', *, *, #3666, .T. ) ;
#5785=AXIS2_PLACEMENT_3D ( 'NONE', #4110, #4186, #2351 ) ;
#5817=CARTESIAN_POINT ( 'NONE',  ( 340.0000000000000000, -12.50000000000000355, -15.61249499599599311 ) ) ;
#5829=CARTESIAN_POINT ( 'NONE',  ( 382.6415087606284828, 17.37175308249308969, 9.924386979199645964 ) ) ;
#5847=ORIENTED_EDGE ( 'NONE', *, *, #5719, .F. ) ;
#5859=EDGE_CURVE ( 'NONE', #5409, #3124, #1132, .T. ) ;
#5864=DIRECTION ( 'NONE',  ( 0.000000000000000000, 0.000000000000000000, 1.000000000000000000 ) ) ;
#5867=CARTESIAN_POINT ( 'NONE',  ( 386.6668409306243461, 19.48969576164946105, 4.506197270647787967 ) ) ;
#5873=ORIENTED_EDGE ( 'NONE', *, *, #4090, .F. ) ;
#5878=DIRECTION ( 'NONE',  ( 0.000000000000000000, -1.000000000000000000, 0.000000000000000000 ) ) ;
#5881=VECTOR ( 'NONE', #239, 1000.000000000000114 ) ;
#5882=ORIENTED_EDGE ( 'NONE', *, *, #5962, .F. ) ;
#5900=DIRECTION ( 'NONE',  ( -1.000000000000000000, -0.000000000000000000, -0.000000000000000000 ) ) ;
#5932=FACE_OUTER_BOUND ( 'NONE', #493, .T. ) ;
#5933=EDGE_LOOP ( 'NONE', ( #1920, #1907, #5580, #529 ) ) ;
#5950=CARTESIAN_POINT ( 'NONE',  ( 398.0000000000001137, -12.50000000000000000, 15.61249499599599488 ) ) ;
#5961=VERTEX_POINT ( 'NONE', #1331 ) ;
#5962=EDGE_CURVE ( 'NONE', #6439, #6900, #6257, .T. ) ;
#5969=EDGE_CURVE ( 'NONE', #7097, #5961, #5510, .T. ) ;
#5975=ORIENTED_EDGE ( 'NONE', *, *, #6796, .F. ) ;
#5978=CARTESIAN_POINT ( 'NONE',  ( 398.0000000000001137, 0.000000000000000000, 0.000000000000000000 ) ) ;
#5979=CARTESIAN_POINT ( 'NONE',  ( 398.0000000000001137, 0.000000000000000000, 0.000000000000000000 ) ) ;
#5989=CARTESIAN_POINT ( 'NONE',  ( 381.3287739023131735, 16.83573837738345702, -10.80867071580873784 ) ) ;
#5990=AXIS2_PLACEMENT_3D ( 'NONE', #7897, #1807, #2302 ) ;
#6017=CARTESIAN_POINT ( 'NONE',  ( 367.3650727329744541, -17.37719324208310923, -9.905392396107414399 ) ) ;
#6026=CARTESIAN_POINT ( 'NONE',  ( 375.8509803977445927, -15.63011725355127624, 12.47807683047398619 ) ) ;
#6029=CARTESIAN_POINT ( 'NONE',  ( 400.0000000000000000, -12.50000000000000000, 25.00000000000000000 ) ) ;
#6031=DIRECTION ( 'NONE',  ( -1.000000000000000000, -0.000000000000000000, -0.000000000000000000 ) ) ;
#6032=CARTESIAN_POINT ( 'NONE',  ( 386.6774787981661348, 19.49607926063143282, -4.478210459206754201 ) ) ;
#6038=PLANE ( 'NONE',  #7861 ) ;
#6046=DIRECTION ( 'NONE',  ( 0.000000000000000000, 0.000000000000000000, 1.000000000000000000 ) ) ;
#6054=CARTESIAN_POINT ( 'NONE',  ( 365.6270046772841624, -18.20868245435311295, 8.279865652961362343 ) ) ;
#6057=DIRECTION ( 'NONE',  ( -1.000000000000000000, -0.000000000000000000, -0.000000000000000000 ) ) ;
#6080=ORIENTED_EDGE ( 'NONE', *, *, #2685, .T. ) ;
#6095=CARTESIAN_POINT ( 'NONE',  ( 371.6755651776492186, -15.95794361973645792, -12.05683462702026176 ) ) ;
#6109=CARTESIAN_POINT ( 'NONE',  ( 384.3951573019774628, 18.21476284106545052, -8.283543559714008353 ) ) ;
#6128=CIRCLE ( 'NONE', #758, 18.00000000000007105 ) ;
#6130=CARTESIAN_POINT ( 'NONE',  ( 370.8878672368923048, 16.14034269873396710, 11.81156333678811876 ) ) ;
#6132=CARTESIAN_POINT ( 'NONE',  ( 370.5028268974027696, -16.24331487217730796, -11.67016537472322746 ) ) ;
#6152=CARTESIAN_POINT ( 'NONE',  ( 325.0000000000000000, -12.50000000000000000, 21.65063509461096913 ) ) ;
#6169=EDGE_CURVE ( 'NONE', #5516, #7370, #1726, .T. ) ;
#6170=CARTESIAN_POINT ( 'NONE',  ( 370.5038504081379642, 16.24311277381278984, 11.67040959636601016 ) ) ;
#6173=CARTESIAN_POINT ( 'NONE',  ( 362.5817914570322387, -19.94855572367474750, -1.655112461855906769 ) ) ;
#6183=CARTESIAN_POINT ( 'NONE',  ( 379.4961495918622632, -16.24311277381278984, 11.67040959636601016 ) ) ;
#6187=DIRECTION ( 'NONE',  ( 0.000000000000000000, 0.000000000000000000, -1.000000000000000000 ) ) ;
#6192=DIRECTION ( 'NONE',  ( 0.000000000000000000, 1.000000000000000000, 0.000000000000000000 ) ) ;
#6194=FACE_BOUND ( 'NONE', #7648, .T. ) ;
#6197=ORIENTED_EDGE ( 'NONE', *, *, #1980, .F. ) ;
#6208=CARTESIAN_POINT ( 'NONE',  ( 367.3565110264916029, 17.37246880845878039, -9.923319895790875478 ) ) ;
#6221=ORIENTED_EDGE ( 'NONE', *, *, #6916, .T. ) ;
#6228=ADVANCED_FACE ( 'NONE', ( #7227 ), #5372, .F. ) ;
#6235=ORIENTED_EDGE ( 'NONE', *, *, #1766, .T. ) ;
#6239=DIRECTION ( 'NONE',  ( -1.000000000000000000, -0.000000000000000000, -0.000000000000000000 ) ) ;
#6240=VERTEX_POINT ( 'NONE', #5382 ) ;
#6245=CARTESIAN_POINT ( 'NONE',  ( 340.0000000000000000, 0.000000000000000000, 0.000000000000000000 ) ) ;
#6246=EDGE_LOOP ( 'NONE', ( #5873, #6859, #4746, #2038, #1422, #5353, #5522, #215 ) ) ;
#6257=CIRCLE ( 'NONE', #508, 25.00000000000000000 ) ;
#6276=VERTEX_POINT ( 'NONE', #4690 ) ;
#6284=CARTESIAN_POINT ( 'NONE',  ( 373.3169687445243312, 15.68244000841234964, -12.41390036673199759 ) ) ;
#6299=DIRECTION ( 'NONE',  ( 0.000000000000000000, 0.000000000000000000, -1.000000000000000000 ) ) ;
#6305=CARTESIAN_POINT ( 'NONE',  ( 375.0000000000000000, 12.50000000000000000, -12.50000000000000000 ) ) ;
#6337=CARTESIAN_POINT ( 'NONE',  ( 175.0000000000000000, 0.000000000000000000, 15.00000000000000000 ) ) ;
#6344=LINE ( 'NONE', #2051, #6973 ) ;
#6386=FACE_BOUND ( 'NONE', #775, .T. ) ;
#6403=ORIENTED_EDGE ( 'NONE', *, *, #3507, .T. ) ;
#6409=EDGE_CURVE ( 'NONE', #2643, #4500, #5635, .T. ) ;
#6428=CARTESIAN_POINT ( 'NONE',  ( 190.0000000000000000, 12.50000000000000000, -15.61249499599599488 ) ) ;
#6434=APPLICATION_CONTEXT ( 'automotive_design' ) ;
#6439=VERTEX_POINT ( 'NONE', #4253 ) ;
#6451=AXIS2_PLACEMENT_3D ( 'NONE', #5191, #7688, #349 ) ;
#6452=DIRECTION ( 'NONE',  ( 1.000000000000000000, 0.000000000000000000, 0.000000000000000000 ) ) ;
#6461=CIRCLE ( 'NONE', #3014, 18.00000000000007105 ) ;
#6480=EDGE_CURVE ( 'NONE', #1507, #4567, #6528, .T. ) ;
#6487=CARTESIAN_POINT ( 'NONE',  ( 6.249999999999977796, 3.061616997868383043E-15, -25.00000000000000000 ) ) ;
#6490=DIRECTION ( 'NONE',  ( -1.000000000000000000, -0.000000000000000000, -0.000000000000000000 ) ) ;
#6505=EDGE_CURVE ( 'NONE', #4567, #1507, #249, .T. ) ;
#6507=EDGE_CURVE ( 'NONE', #6766, #6240, #7580, .T. ) ;
#6528=CIRCLE ( 'NONE', #7295, 12.50000000000000355 ) ;
#6542=CARTESIAN_POINT ( 'NONE',  ( 400.0000000000000000, 0.000000000000000000, 0.000000000000000000 ) ) ;
#6544=ORIENTED_EDGE ( 'NONE', *, *, #1165, .T. ) ;
#6555=CARTESIAN_POINT ( 'NONE',  ( 0.000000000000000000, 1.836970198721029589E-15, -15.00000000000000000 ) ) ;
#6561=VERTEX_POINT ( 'NONE', #2651 ) ;
#6562=EDGE_CURVE ( 'NONE', #3264, #136, #3372, .T. ) ;
#6566=DIRECTION ( 'NONE',  ( 0.000000000000000000, 0.000000000000000000, 1.000000000000000000 ) ) ;
#6569=DIRECTION ( 'NONE',  ( 0.000000000000000000, 0.000000000000000000, 1.000000000000000000 ) ) ;
#6571=ORIENTED_EDGE ( 'NONE', *, *, #4090, .T. ) ;
#6572=LINE ( 'NONE', #4120, #2816 ) ;
#6575=ORIENTED_EDGE ( 'NONE', *, *, #7296, .F. ) ;
#6596=DIRECTION ( 'NONE',  ( 0.000000000000000000, -1.000000000000000000, 0.000000000000000000 ) ) ;
#6598=CIRCLE ( 'NONE', #2369, 20.00000000000000000 ) ;
#6599=ADVANCED_FACE ( 'NONE', ( #4724 ), #5615, .T. ) ;
#6608=CARTESIAN_POINT ( 'NONE',  ( 190.0000000000000000, 0.000000000000000000, 0.000000000000000000 ) ) ;
#6616=CARTESIAN_POINT ( 'NONE',  ( 362.8413258170837707, -19.78835583758980832, 2.930536303278098664 ) ) ;
#6621=ORIENTED_EDGE ( 'NONE', *, *, #6169, .F. ) ;
#6629=CARTESIAN_POINT ( 'NONE',  ( 380.6272118725746623, 16.58005916595991280, -11.19168395254304471 ) ) ;
#6640=EDGE_CURVE ( 'NONE', #5516, #7370, #6128, .T. ) ;
#6657=CARTESIAN_POINT ( 'NONE',  ( 363.8177372226678017, -19.20332549959546853, -5.601192942097885208 ) ) ;
#6665=LINE ( 'NONE', #7789, #86 ) ;
#6682=CYLINDRICAL_SURFACE ( 'NONE', #3645, 25.00000000000000000 ) ;
#6690=CARTESIAN_POINT ( 'NONE',  ( 366.7466773492281504, -17.65289753843946841, 9.421765557058566998 ) ) ;
#6717=CARTESIAN_POINT ( 'NONE',  ( 375.0000000000000000, -12.50000000000000355, 12.50000000000000711 ) ) ;
#6727=CARTESIAN_POINT ( 'NONE',  ( 362.6036394379159447, 19.93536271250352598, 1.660494579713906127 ) ) ;
#6729=CARTESIAN_POINT ( 'NONE',  ( 363.6408507984733660, -19.30709367143974831, -5.233317247790644444 ) ) ;
#6736=CIRCLE ( 'NONE', #2899, 18.75000000000009948 ) ;
#6737=ORIENTED_EDGE ( 'NONE', *, *, #2046, .T. ) ;
#6741=CARTESIAN_POINT ( 'NONE',  ( 387.0561628848909663, -19.72539574521466932, -3.327763323014857555 ) ) ;
#6753=CARTESIAN_POINT ( 'NONE',  ( 190.0000000000000000, -12.50000000000000000, -21.65063509461096913 ) ) ;
#6766=VERTEX_POINT ( 'NONE', #5407 ) ;
#6768=STYLED_ITEM('',(#7962),#6795);
#6774=CARTESIAN_POINT ( 'NONE',  ( 362.5234216988060894, -19.98534102192048323, 0.8725863811532602599 ) ) ;
#6782=ORIENTED_EDGE ( 'NONE', *, *, #5133, .T. ) ;
#6786=CARTESIAN_POINT ( 'NONE',  ( 375.0000000000000000, 12.50000000000000000, 3.061616997868383043E-15 ) ) ;
#6795=MANIFOLD_SOLID_BREP ( 'Pah2', #566 ) ;
#6796=EDGE_CURVE ( 'NONE', #2057, #7215, #31, .T. ) ;
#6809=PLANE ( 'NONE',  #1783 ) ;
#6822=CARTESIAN_POINT ( 'NONE',  ( 386.6750961250273235, -19.49464854461726304, 4.484522112394339288 ) ) ;
#6830=FACE_OUTER_BOUND ( 'NONE', #5933, .T. ) ;
#6835=ORIENTED_EDGE ( 'NONE', *, *, #2573, .T. ) ;
#6849=CARTESIAN_POINT ( 'NONE',  ( 363.3249038749727333, 19.49464854461726304, 4.484522112394339288 ) ) ;
#6859=ORIENTED_EDGE ( 'NONE', *, *, #1587, .T. ) ;
#6864=CARTESIAN_POINT ( 'NONE',  ( 378.3038998296499926, -15.95358756117676258, -12.06260739558933714 ) ) ;
#6878=LINE ( 'NONE', #3904, #5357 ) ;
#6884=CARTESIAN_POINT ( 'NONE',  ( 381.6490413535094035, 16.96668907523693548, 10.59241602951089867 ) ) ;
#6888=CARTESIAN_POINT ( 'NONE',  ( 363.8044315608395323, 19.21001202690979781, 5.620007094727602848 ) ) ;
#6892=CARTESIAN_POINT ( 'NONE',  ( 190.0000000000000000, -12.50000000000000000, -15.61249499599599488 ) ) ;
#6900=VERTEX_POINT ( 'NONE', #1949 ) ;
#6905=CARTESIAN_POINT ( 'NONE',  ( 387.1601938586447318, -19.78928940797825931, -2.924464941254242056 ) ) ;
#6908=ADVANCED_FACE ( 'NONE', ( #3208, #1354 ), #5653, .F. ) ;
#6912=FACE_OUTER_BOUND ( 'NONE', #5184, .T. ) ;
#6916=EDGE_CURVE ( 'NONE', #4834, #1320, #4434, .T. ) ;
#6920=ORIENTED_EDGE ( 'NONE', *, *, #5117, .T. ) ;
#6957=CARTESIAN_POINT ( 'NONE',  ( 325.0000000000000000, 12.50000000000000000, 25.00000000000000000 ) ) ;
#6973=VECTOR ( 'NONE', #7624, 1000.000000000000000 ) ;
#6990=FACE_OUTER_BOUND ( 'NONE', #2559, .T. ) ;
#7006=ORIENTED_EDGE ( 'NONE', *, *, #3675, .T. ) ;
#7036=AXIS2_PLACEMENT_3D ( 'NONE', #6245, #710, #2594 ) ;
#7037=AXIS2_PLACEMENT_3D ( 'NONE', #1089, #3419, #5864 ) ;
#7049=CYLINDRICAL_SURFACE ( 'NONE', #2514, 12.50000000000000355 ) ;
#7050=FACE_OUTER_BOUND ( 'NONE', #5076, .T. ) ;
#7062=DIRECTION ( 'NONE',  ( -1.000000000000000000, -0.000000000000000000, -0.000000000000000000 ) ) ;
#7066=EDGE_CURVE ( 'NONE', #7370, #4834, #5388, .T. ) ;
#7071=CARTESIAN_POINT ( 'NONE',  ( 384.8819872053468885, 18.47584224143657039, 7.665216593424116986 ) ) ;
#7078=EDGE_LOOP ( 'NONE', ( #6621, #7662 ) ) ;
#7084=ORIENTED_EDGE ( 'NONE', *, *, #900, .F. ) ;
#7087=ORIENTED_EDGE ( 'NONE', *, *, #5133, .F. ) ;
#7097=VERTEX_POINT ( 'NONE', #5674 ) ;
#7101=EDGE_CURVE ( 'NONE', #1578, #1, #6878, .T. ) ;
#7102=VECTOR ( 'NONE', #926, 1000.000000000000000 ) ;
#7121=FACE_OUTER_BOUND ( 'NONE', #4206, .T. ) ;
#7140=ORIENTED_EDGE ( 'NONE', *, *, #4971, .T. ) ;
#7157=VECTOR ( 'NONE', #465, 1000.000000000000000 ) ;
#7166=EDGE_CURVE ( 'NONE', #2585, #1234, #5673, .T. ) ;
#7172=ORIENTED_EDGE ( 'NONE', *, *, #4645, .F. ) ;
#7196=CARTESIAN_POINT ( 'NONE',  ( 387.0648300283518211, 19.73070161726337446, -3.295910870315892804 ) ) ;
#7208=ORIENTED_EDGE ( 'NONE', *, *, #6409, .F. ) ;
#7215=VERTEX_POINT ( 'NONE', #6555 ) ;
#7218=ORIENTED_EDGE ( 'NONE', *, *, #4236, .F. ) ;
#7219=CARTESIAN_POINT ( 'NONE',  ( 362.9446671282877332, -19.72489609666084576, 3.330011984645298462 ) ) ;
#7224=CIRCLE ( 'NONE', #1199, 15.00000000000000000 ) ;
#7226=DIRECTION ( 'NONE',  ( -1.000000000000000000, -0.000000000000000000, -0.000000000000000000 ) ) ;
#7227=FACE_OUTER_BOUND ( 'NONE', #3205, .T. ) ;
#7232=CARTESIAN_POINT ( 'NONE',  ( 382.3165647940696203, 17.23925164521633846, -10.14275924251023220 ) ) ;
#7248=VERTEX_POINT ( 'NONE', #2343 ) ;
#7260=CARTESIAN_POINT ( 'NONE',  ( 363.1903364394804044, -19.57571528166833019, 4.117265725333339788 ) ) ;
#7263=CARTESIAN_POINT ( 'NONE',  ( 400.0000000000000000, 0.000000000000000000, 0.000000000000000000 ) ) ;
#7295=AXIS2_PLACEMENT_3D ( 'NONE', #6786, #3745, #6187 ) ;
#7296=EDGE_CURVE ( 'NONE', #2321, #5516, #3288, .T. ) ;
#7299=ORIENTED_EDGE ( 'NONE', *, *, #2971, .T. ) ;
#7301=CARTESIAN_POINT ( 'NONE',  ( 369.7712349971211552, -16.46093790404528789, 11.36110438390628197 ) ) ;
#7314=CARTESIAN_POINT ( 'NONE',  ( 387.4182085429678750, 19.94855572367474750, -1.655112461855906769 ) ) ;
#7325=DIRECTION ( 'NONE',  ( 1.000000000000000000, 0.000000000000000000, 0.000000000000000000 ) ) ;
#7335=CARTESIAN_POINT ( 'NONE',  ( 375.0000000000000000, 15.61249499599599488, -12.50000000000000000 ) ) ;
#7343=ORIENTED_EDGE ( 'NONE', *, *, #1766, .F. ) ;
#7356=PLANE ( 'NONE',  #1109 ) ;
#7370=VERTEX_POINT ( 'NONE', #194 ) ;
#7372=UNCERTAINTY_MEASURE_WITH_UNIT (LENGTH_MEASURE( 1.000000000000000082E-05 ), #2445, 'distance_accuracy_value', 'NONE');
#7375=CARTESIAN_POINT ( 'NONE',  ( 362.5018422615490294, 19.99884858813039301, -0.8730781214943976742 ) ) ;
#7377=CARTESIAN_POINT ( 'NONE',  ( 375.0000000000000000, -15.61249499599599488, -12.50000000000000000 ) ) ;
#7379=( NAMED_UNIT ( * ) PLANE_ANGLE_UNIT ( ) SI_UNIT ( $, .RADIAN. ) );
#7388=CARTESIAN_POINT ( 'NONE',  ( 385.7978869038915946, -18.97902931052027142, -6.348195341973490891 ) ) ;
#7393=AXIS2_PLACEMENT_3D ( 'NONE', #1105, #7325, #1748 ) ;
#7397=DIRECTION ( 'NONE',  ( 0.000000000000000000, 0.000000000000000000, -1.000000000000000000 ) ) ;
#7401=AXIS2_PLACEMENT_3D ( 'NONE', #4336, #1369, #1330 ) ;
#7414=CARTESIAN_POINT ( 'NONE',  ( 366.4564998757169292, 17.79554561421092984, 9.133253117746194860 ) ) ;
#7442=( NAMED_UNIT ( * ) PLANE_ANGLE_UNIT ( ) SI_UNIT ( $, .RADIAN. ) );
#7452=CARTESIAN_POINT ( 'NONE',  ( 363.1816593327628198, 19.58094920198549360, 4.092816503359988367 ) ) ;
#7473=ORIENTED_EDGE ( 'NONE', *, *, #2332, .T. ) ;
#7485=CONICAL_SURFACE ( 'NONE', #1965, 20.00000000000000000, 0.7853981633974578269 ) ;
#7487=EDGE_CURVE ( 'NONE', #3245, #4927, #1555, .T. ) ;
#7491=CYLINDRICAL_SURFACE ( 'NONE', #4936, 12.50000000000000355 ) ;
#7504=CARTESIAN_POINT ( 'NONE',  ( 384.0988265331048410, -18.06872101906905215, -8.580138959277956445 ) ) ;
#7544=CARTESIAN_POINT ( 'NONE',  ( 398.0000000000001137, 12.50000000000000000, -15.61249499599599488 ) ) ;
#7545=ORIENTED_EDGE ( 'NONE', *, *, #7765, .F. ) ;
#7576=ORIENTED_EDGE ( 'NONE', *, *, #4211, .F. ) ;
#7580=LINE ( 'NONE', #6337, #359 ) ;
#7583=EDGE_LOOP ( 'NONE', ( #594, #1147 ) ) ;
#7596=EDGE_CURVE ( 'NONE', #4834, #2321, #2844, .T. ) ;
#7624=DIRECTION ( 'NONE',  ( 0.000000000000000000, 0.000000000000000000, 1.000000000000000000 ) ) ;
#7648=EDGE_LOOP ( 'NONE', ( #5278, #635 ) ) ;
#7653=DIRECTION ( 'NONE',  ( 0.000000000000000000, 0.000000000000000000, -1.000000000000000000 ) ) ;
#7662=ORIENTED_EDGE ( 'NONE', *, *, #6640, .T. ) ;
#7669=VECTOR ( 'NONE', #534, 1000.000000000000000 ) ;
#7678=CARTESIAN_POINT ( 'NONE',  ( 190.0000000000000000, -12.50000000000000000, 15.61249499599599488 ) ) ;
#7682=EDGE_CURVE ( 'NONE', #4500, #4609, #6572, .T. ) ;
#7684=FACE_BOUND ( 'NONE', #5316, .T. ) ;
#7685=ORIENTED_EDGE ( 'NONE', *, *, #7487, .T. ) ;
#7688=DIRECTION ( 'NONE',  ( -1.000000000000000000, -0.000000000000000000, -0.000000000000000000 ) ) ;
#7689=ORIENTED_EDGE ( 'NONE', *, *, #5037, .T. ) ;
#7692=ORIENTED_EDGE ( 'NONE', *, *, #4491, .F. ) ;
#7706=CARTESIAN_POINT ( 'NONE',  ( 6.249999999999977796, 0.000000000000000000, 0.000000000000000000 ) ) ;
#7710=CARTESIAN_POINT ( 'NONE',  ( 387.0553328717124941, 19.72489609666084576, 3.330011984645298462 ) ) ;
#7711=CARTESIAN_POINT ( 'NONE',  ( 398.0000000000001137, 12.50000000000000000, 15.61249499599599488 ) ) ;
#7731=ORIENTED_EDGE ( 'NONE', *, *, #3219, .T. ) ;
#7736=CYLINDRICAL_SURFACE ( 'NONE', #7766, 15.00000000000000000 ) ;
#7765=EDGE_CURVE ( 'NONE', #1377, #322, #2554, .T. ) ;
#7766=AXIS2_PLACEMENT_3D ( 'NONE', #2249, #2893, #4680 ) ;
#7770=CARTESIAN_POINT ( 'NONE',  ( 325.0000000000000000, 12.50000000000000000, 25.00000000000000000 ) ) ;
#7776=EDGE_CURVE ( 'NONE', #3409, #968, #772, .T. ) ;
#7787=ORIENTED_EDGE ( 'NONE', *, *, #68, .T. ) ;
#7789=CARTESIAN_POINT ( 'NONE',  ( 190.0000000000000000, 0.000000000000000000, 25.00000000000000000 ) ) ;
#7790=ADVANCED_FACE ( 'NONE', ( #3126 ), #6809, .F. ) ;
#7794=CARTESIAN_POINT ( 'NONE',  ( 375.0000000000000000, 15.61249499599599488, 12.50000000000000711 ) ) ;
#7795=AXIS2_PLACEMENT_3D ( 'NONE', #6957, #1457, #5138 ) ;
#7813=CARTESIAN_POINT ( 'NONE',  ( 0.000000000000000000, 2.678914873134841621E-15, 18.75000000000009948 ) ) ;
#7825=ADVANCED_FACE ( 'NONE', ( #7684, #5143 ), #2714, .T. ) ;
#7826=CARTESIAN_POINT ( 'NONE',  ( 398.0000000000001137, -12.50000000000000000, -15.61249499599599488 ) ) ;
#7831=CARTESIAN_POINT ( 'NONE',  ( 386.1822627773321415, 19.20332549959546853, -5.601192942097885208 ) ) ;
#7833=ADVANCED_FACE ( 'NONE', ( #985 ), #2836, .F. ) ;
#7850=CARTESIAN_POINT ( 'NONE',  ( 374.5751407255119716, -15.61249499599599666, -12.50000000000000000 ) ) ;
#7855=VECTOR ( 'NONE', #1150, 1000.000000000000000 ) ;
#7861=AXIS2_PLACEMENT_3D ( 'NONE', #2870, #1139, #5390 ) ;
#7866=VECTOR ( 'NONE', #3224, 1000.000000000000000 ) ;
#7873=CIRCLE ( 'NONE', #4409, 15.00000000000000000 ) ;
#7888=CARTESIAN_POINT ( 'NONE',  ( 373.3039311335094794, -15.69870025322426699, -12.39168528959425331 ) ) ;
#7896=CARTESIAN_POINT ( 'NONE',  ( 381.3155148028032499, -16.83062759343247805, 10.81672997705310557 ) ) ;
#7897=CARTESIAN_POINT ( 'NONE',  ( 0.000000000000000000, 0.000000000000000000, 0.000000000000000000 ) ) ;
#7901=B_SPLINE_CURVE_WITH_KNOTS ( 'NONE', 3,
 ( #763, #122, #160, #2568, #6864, #3215, #3064, #5660, #682, #4973, #2606, #7504, #3138, #1923, #4290, #7388, #2002, #725, #1404, #6741, #6905, #611, #1247, #3704, #5538, #3744, #2492, #4932, #4326, #4365, #6822, #1323, #3020, #3743, #5536, #1168, #3101, #570, #610, #7896, #3616, #6183, #2370, #681, #3137, #2413, #37, #6026, #3, #4807 ),
 .UNSPECIFIED., .F., .F.,
 ( 4, 2, 2, 2, 2, 2, 2, 2, 2, 2, 2, 2, 2, 2, 2, 2, 2, 2, 2, 2, 2, 2, 2, 2, 4 ),
 ( 0.000000000000000000, 0.002511627799209755017, 0.003767441698814711672, 0.005023255598419669628, 0.007534883397629582938, 0.01004651119683949712, 0.01130232509644451058, 0.01255813899604952405, 0.01506976679525946078, 0.01632558069486442914, 0.01758139459446940098, 0.02009302239367936893, 0.02134883629328435117, 0.02260465019288934035, 0.02386046409249432260, 0.02511627799209930484, 0.02762790579130921381, 0.03013953359051911585, 0.03139534749012407033, 0.03265116138972902482, 0.03516278918893894073, 0.03641860308854381889, 0.03767441698814869705, 0.03893023088775358215, 0.04018604478735846031 ),
 .UNSPECIFIED. ) ;
#7903=CARTESIAN_POINT ( 'NONE',  ( 378.3244348223507245, 15.95794361973645792, -12.05683462702026176 ) ) ;
#7956=COLOUR_RGB('Grey',0.48,0.52,0.57);
#7957=FILL_AREA_STYLE_COLOUR('',#7956);
#7958=FILL_AREA_STYLE('',(#7957));
#7959=SURFACE_STYLE_FILL_AREA(#7958);
#7960=SURFACE_SIDE_STYLE('',(#7959));
#7961=SURFACE_STYLE_USAGE(.BOTH.,#7960);
#7962=PRESENTATION_STYLE_ASSIGNMENT((#7961));
ENDSEC;
END-ISO-10303-21;
